ISO-10303-21;
HEADER;
FILE_DESCRIPTION (('STEP AP214'),
    '1' );
FILE_NAME ('hex flange nut gradea_iso_ISO - 4161 - M5 - N.step',
    '2026-10-24T13:33:06',
    ( '' ),
    ( '' ),
    'SwSTEP 2.0',
    'SolidWorks 2026',
    '' );
FILE_SCHEMA (( 'AUTOMOTIVE_DESIGN' ));
ENDSEC;

DATA;
#6=DIRECTION ( 'NONE',  ( 0.000000000000000000, 0.000000000000000000, -1.000000000000000000 ) ) ;
#27=DIRECTION ( 'NONE',  ( -0.000000000000000000, 0.000000000000000000, -1.000000000000000000 ) ) ;
#32=VERTEX_POINT ( 'NONE', #10617 ) ;
#38=CARTESIAN_POINT ( 'NONE',  ( 4.175648173966055587, -2.207990556236547608, -3.469390959564065291 ) ) ;
#55=ORIENTED_EDGE ( 'NONE', *, *, #9775, .T. ) ;
#60=CARTESIAN_POINT ( 'NONE',  ( 4.000000000000000000, 2.309401076758497151, -3.433295621305379353 ) ) ;
#102=ORIENTED_EDGE ( 'NONE', *, *, #13999, .T. ) ;
#126=CARTESIAN_POINT ( 'NONE',  ( 4.000000000000000888, 1.539600717838996990, -3.300726591567079815 ) ) ;
#139=B_SPLINE_CURVE_WITH_KNOTS ( 'NONE', 3,
 ( #12728, #3886, #6926, #516, #12587, #8082 ),
 .UNSPECIFIED., .F., .F.,
 ( 4, 2, 4 ),
 ( 0.002365888236227967761, 0.003551327329835077609, 0.004736766423442186590 ),
 .UNSPECIFIED. ) ;
#174=B_SPLINE_CURVE_WITH_KNOTS ( 'NONE', 3,
 ( #13860, #2775, #7121, #12779, #11548 ),
 .UNSPECIFIED., .F., .F.,
 ( 4, 1, 4 ),
 ( 0.000000000000000000, 0.002309401076758506657, 0.004618802153517013315 ),
 .UNSPECIFIED. ) ;
#189=CARTESIAN_POINT ( 'NONE',  ( 4.207491450040567571, -2.029819825146485179, -3.671670828759567407 ) ) ;
#213=CARTESIAN_POINT ( 'NONE',  ( 3.383466608491643077E-15, 4.736522675502341073, -3.681124513963742739 ) ) ;
#243=CARTESIAN_POINT ( 'NONE',  ( 4.141042297810615835, -2.227970268150433863, -3.687027686973623819 ) ) ;
#249=CARTESIAN_POINT ( 'NONE',  ( 2.756197834950227410, 3.027510591568626896, -3.223146290109805356 ) ) ;
#253=CARTESIAN_POINT ( 'NONE',  ( -2.000000000000002665, -3.464101615137770374, -3.142992957459237680 ) ) ;
#271=FACE_OUTER_BOUND ( 'NONE', #11503, .T. ) ;
#360=DIRECTION ( 'NONE',  ( -1.000000000000000000, 0.000000000000000000, 0.000000000000000000 ) ) ;
#376=PLANE ( 'NONE',  #9014 ) ;
#389=CARTESIAN_POINT ( 'NONE',  ( 0.000000000000000000, 0.000000000000000000, -0.2800830152838844622 ) ) ;
#416=ADVANCED_FACE ( 'NONE', ( #1651, #7249 ), #6159, .T. ) ;
#431=AXIS2_PLACEMENT_3D ( 'NONE', #11953, #12886, #4331 ) ;
#447=CIRCLE ( 'NONE', #4421, 2.100000000000000089 ) ;
#449=LINE ( 'NONE', #13747, #10932 ) ;
#460=ORIENTED_EDGE ( 'NONE', *, *, #9965, .F. ) ;
#478=CARTESIAN_POINT ( 'NONE',  ( 2.691179338796023329E-15, 4.647089433458991614, -3.572167766733753691 ) ) ;
#484=CARTESIAN_POINT ( 'NONE',  ( 0.000000000000000000, 0.000000000000000000, -4.974599999999998801 ) ) ;
#490=SURFACE_STYLE_USAGE ( .BOTH. , #3852 ) ;
#516=CARTESIAN_POINT ( 'NONE',  ( 0.6507732100473444525, -4.243078065514795050, -0.2236248678334952777 ) ) ;
#557=CARTESIAN_POINT ( 'NONE',  ( -4.000000000000000000, 0.7924765000094600165, -0.05906175389889745803 ) ) ;
#564=FACE_OUTER_BOUND ( 'NONE', #5808, .T. ) ;
#579=DIRECTION ( 'NONE',  ( 0.000000000000000000, 0.000000000000000000, -1.000000000000000000 ) ) ;
#591=CARTESIAN_POINT ( 'NONE',  ( 0.000000000000000000, 0.000000000000000000, 0.000000000000000000 ) ) ;
#594=ORIENTED_EDGE ( 'NONE', *, *, #14027, .F. ) ;
#596=VECTOR ( 'NONE', #756, 999.9999999999998863 ) ;
#602=CARTESIAN_POINT ( 'NONE',  ( 0.000000000000000000, 0.000000000000000000, -0.3080913168122742518 ) ) ;
#628=DIRECTION ( 'NONE',  ( 0.000000000000000000, 0.000000000000000000, -1.000000000000000000 ) ) ;
#646=ORIENTED_EDGE ( 'NONE', *, *, #7816, .F. ) ;
#650=CARTESIAN_POINT ( 'NONE',  ( 2.171643655288379993, -3.365003104552334978, -1.195831703456429434E-14 ) ) ;
#664=ORIENTED_EDGE ( 'NONE', *, *, #6928, .F. ) ;
#676=CARTESIAN_POINT ( 'NONE',  ( 0.000000000000000000, 0.000000000000000000, -25.03750572909317285 ) ) ;
#692=EDGE_LOOP ( 'NONE', ( #5949, #6381, #4636, #10880 ) ) ;
#697=DIRECTION ( 'NONE',  ( 1.224646799147353207E-16, 1.000000000000000000, 0.000000000000000000 ) ) ;
#706=CARTESIAN_POINT ( 'NONE',  ( -4.211140560182196957, -2.431303136016552013, -3.745885042887436178 ) ) ;
#714=ORIENTED_EDGE ( 'NONE', *, *, #5887, .F. ) ;
#745=CARTESIAN_POINT ( 'NONE',  ( 4.000000000000000000, 0.000000000000000000, 0.000000000000000000 ) ) ;
#756=DIRECTION ( 'NONE',  ( 0.8191520442889875797, 0.000000000000000000, 0.5735764363510522656 ) ) ;
#760=CARTESIAN_POINT ( 'NONE',  ( 4.000000000000000000, -2.471525695159793035, -3.686886880705770864 ) ) ;
#771=CARTESIAN_POINT ( 'NONE',  ( -4.197393957002303999, 0.4069871074557429025, -3.503767560748926257 ) ) ;
#802=EDGE_CURVE ( 'NONE', #6984, #1149, #10339, .T. ) ;
#834=CARTESIAN_POINT ( 'NONE',  ( 4.000000000000000000, 0.8378280264232961239, -3.220590601395640018 ) ) ;
#864=CONICAL_SURFACE ( 'NONE', #7822, 4.000000000000000000, 0.8911886515913786111 ) ;
#890=CARTESIAN_POINT ( 'NONE',  ( -4.024497503033714452, -2.323544716729502468, -3.572167766733752803 ) ) ;
#894=EDGE_CURVE ( 'NONE', #12837, #2710, #6725, .T. ) ;
#911=ORIENTED_EDGE ( 'NONE', *, *, #13115, .T. ) ;
#922=CARTESIAN_POINT ( 'NONE',  ( -4.000000000000000000, 2.511478553582031203, -3.469254451724764543 ) ) ;
#924=VERTEX_POINT ( 'NONE', #12743 ) ;
#931=VERTEX_POINT ( 'NONE', #8233 ) ;
#946=CIRCLE ( 'NONE', #11369, 4.000000000000000000 ) ;
#952=CARTESIAN_POINT ( 'NONE',  ( -2.100000000000000089, 2.571758278209441957E-16, -5.000000000000000000 ) ) ;
#974=FACE_OUTER_BOUND ( 'NONE', #7536, .T. ) ;
#975=CARTESIAN_POINT ( 'NONE',  ( 4.000000000000000000, -2.309401076758514915, -3.433295621305383349 ) ) ;
#985=CARTESIAN_POINT ( 'NONE',  ( -0.1750025118121544265, -4.719839900820635314, -3.469254087858253399 ) ) ;
#992=B_SPLINE_CURVE_WITH_KNOTS ( 'NONE', 3,
 ( #9994, #2299, #1039, #13579, #10945, #11010 ),
 .UNSPECIFIED., .F., .F.,
 ( 4, 2, 4 ),
 ( 0.003358874760055551890, 0.004541967308452098118, 0.005725059856848645212 ),
 .UNSPECIFIED. ) ;
#1039=CARTESIAN_POINT ( 'NONE',  ( 4.000000000000000000, -1.560351142792952617, -0.2242961665059816367 ) ) ;
#1042=ADVANCED_FACE ( 'NONE', ( #6284 ), #8457, .F. ) ;
#1052=DIRECTION ( 'NONE',  ( -1.000000000000000000, 0.000000000000000000, 0.000000000000000000 ) ) ;
#1067=LINE ( 'NONE', #11036, #3067 ) ;
#1071=CARTESIAN_POINT ( 'NONE',  ( -1.317756351988340180, 3.857995168970202116, -0.04852650426601388955 ) ) ;
#1079=CIRCLE ( 'NONE', #5291, 2.500000000000000888 ) ;
#1084=DIRECTION ( 'NONE',  ( -0.000000000000000000, -0.000000000000000000, 1.000000000000000000 ) ) ;
#1085=CONICAL_SURFACE ( 'NONE', #9208, 4.000000000000000000, 0.8911886515913786111 ) ;
#1115=AXIS2_PLACEMENT_3D ( 'NONE', #7614, #13204, #12122 ) ;
#1149=VERTEX_POINT ( 'NONE', #11481 ) ;
#1161=CARTESIAN_POINT ( 'NONE',  ( 3.999999999999999112, 2.309401076758497595, -3.504271511727124366 ) ) ;
#1206=( GEOMETRIC_REPRESENTATION_CONTEXT ( 3 ) GLOBAL_UNCERTAINTY_ASSIGNED_CONTEXT ( ( #1912 ) ) GLOBAL_UNIT_ASSIGNED_CONTEXT ( ( #12564, #13563, #1591 ) ) REPRESENTATION_CONTEXT ( 'NONE', 'WORKASPACE' ) );
#1237=ADVANCED_FACE ( 'NONE', ( #12422 ), #3096, .F. ) ;
#1241=( BOUNDED_SURFACE ( )  B_SPLINE_SURFACE ( 3, 2, ( 
 ( #1646, #10588, #6229 ),
 ( #1799, #6156, #3983 ),
 ( #9575, #11745, #7310 ),
 ( #13981, #11672, #6086 ),
 ( #2751, #10514, #12754 ),
 ( #8399, #12828, #9425 ) ),
 .UNSPECIFIED., .F., .F., .F. ) 
 B_SPLINE_SURFACE_WITH_KNOTS ( ( 4, 2, 4 ),
 ( 3, 3 ),
 ( 0.02032853247518125531, 0.02278863295364820865, 0.02524873343211516200 ),
 ( 0.000000000000000000, 1.000000000000000000 ),
 .UNSPECIFIED. ) 
 GEOMETRIC_REPRESENTATION_ITEM ( )  RATIONAL_B_SPLINE_SURFACE ( (
 ( 1.000000000000000000, 0.8047781615896836271, 1.000000000000000000),
 ( 1.000000000000000000, 0.8123767586289967202, 1.000000000000000000),
 ( 1.000000000000000000, 0.8190662415563443322, 1.000000000000000000),
 ( 1.000000000000000000, 0.8192361015669982205, 1.000000000000000000),
 ( 1.000000000000000000, 0.8126135807103181952, 1.000000000000000000),
 ( 1.000000000000000000, 0.8047712338318587788, 1.000000000000000000) ) ) 
 REPRESENTATION_ITEM ( '' )  SURFACE ( )  );
#1254=CARTESIAN_POINT ( 'NONE',  ( 4.000000000000000000, 1.680228229147133767, -3.316631783032546021 ) ) ;
#1261=CARTESIAN_POINT ( 'NONE',  ( -2.345747346278108214, 3.264484291692489215, -0.01223254789873409049 ) ) ;
#1268=B_SPLINE_CURVE_WITH_KNOTS ( 'NONE', 3,
 ( #2988, #4066, #5310, #557, #14135, #9731, #10817, #13854 ),
 .UNSPECIFIED., .F., .F.,
 ( 4, 2, 2, 4 ),
 ( 0.005725059856848641743, 0.006314084072593626612, 0.006903108288338611481, 0.008081156719828581220 ),
 .UNSPECIFIED. ) ;
#1274=CIRCLE ( 'NONE', #7988, 5.384454397937118664 ) ;
#1279=DIRECTION ( 'NONE',  ( -0.000000000000000000, -0.000000000000000000, 1.000000000000000000 ) ) ;
#1290=AXIS2_PLACEMENT_3D ( 'NONE', #7574, #8668, #14169 ) ;
#1301=DIRECTION ( 'NONE',  ( 1.000000000000000000, 0.000000000000000000, 0.000000000000000000 ) ) ;
#1307=B_SPLINE_CURVE_WITH_KNOTS ( 'NONE', 3,
 ( #13617, #6813, #253, #11110, #11316 ),
 .UNSPECIFIED., .F., .F.,
 ( 4, 1, 4 ),
 ( 0.000000000000000000, 0.002309401076758505356, 0.004618802153517010713 ),
 .UNSPECIFIED. ) ;
#1335=CARTESIAN_POINT ( 'NONE',  ( -2.171643655288372443, 3.365003104552320767, 2.541098841762897165E-18 ) ) ;
#1345=CIRCLE ( 'NONE', #11564, 0.5155456020628804703 ) ;
#1361=CARTESIAN_POINT ( 'NONE',  ( 4.198928548860774157, -0.8158838809860124996, -3.526471437616918170 ) ) ;
#1385=DIRECTION ( 'NONE',  ( -0.000000000000000000, -0.000000000000000000, 1.000000000000000000 ) ) ;
#1386=B_SPLINE_CURVE_WITH_KNOTS ( 'NONE', 3,
 ( #10306, #4807, #14074, #12843 ),
 .UNSPECIFIED., .F., .F.,
 ( 4, 4 ),
 ( 0.000000000000000000, 0.002452478801916361129 ),
 .UNSPECIFIED. ) ;
#1391=EDGE_CURVE ( 'NONE', #13737, #2488, #10419, .T. ) ;
#1429=CARTESIAN_POINT ( 'NONE',  ( -0.1756481739660520902, 4.720212674038980261, -3.469390959564065291 ) ) ;
#1439=ORIENTED_EDGE ( 'NONE', *, *, #11588, .F. ) ;
#1443=EDGE_LOOP ( 'NONE', ( #5714, #13976, #8402, #3936 ) ) ;
#1469=CARTESIAN_POINT ( 'NONE',  ( 1.567478505476134606E-15, 4.618802153517012066, -5.000000000000000000 ) ) ;
#1480=EDGE_CURVE ( 'NONE', #11371, #2677, #11299, .T. ) ;
#1491=CARTESIAN_POINT ( 'NONE',  ( -0.5449313310646672903, -4.304185902836978883, -3.316620875263469159 ) ) ;
#1494=CARTESIAN_POINT ( 'NONE',  ( -2.059999999999998721, 2.522772406243545965E-16, -0.3080913168122742518 ) ) ;
#1504=AXIS2_PLACEMENT_3D ( 'NONE', #9296, #13632, #11540 ) ;
#1516=CARTESIAN_POINT ( 'NONE',  ( -1.149515148933662080E-15, -4.736529461166056443, -3.681130640444383317 ) ) ;
#1518=( NAMED_UNIT ( * ) SI_UNIT ( $, .STERADIAN. ) SOLID_ANGLE_UNIT ( ) );
#1527=EDGE_CURVE ( 'NONE', #2397, #11346, #11181, .T. ) ;
#1536=VECTOR ( 'NONE', #3721, 1000.000000000000000 ) ;
#1560=CARTESIAN_POINT ( 'NONE',  ( -1.144235203016679359, -3.958177651039096911, -0.09382832055446428676 ) ) ;
#1564=CARTESIAN_POINT ( 'NONE',  ( -1.287237434361707233, -3.875615274277397937, -3.430618716626816500 ) ) ;
#1566=CARTESIAN_POINT ( 'NONE',  ( -5.560781378645575757, 6.809993116116508640E-16, -4.000000000000000000 ) ) ;
#1567=DIRECTION ( 'NONE',  ( 1.000000000000000000, 0.000000000000000000, 0.000000000000000000 ) ) ;
#1570=DIRECTION ( 'NONE',  ( 0.000000000000000000, 0.000000000000000000, -1.000000000000000000 ) ) ;
#1591=( NAMED_UNIT ( * ) SI_UNIT ( $, .STERADIAN. ) SOLID_ANGLE_UNIT ( ) );
#1601=CARTESIAN_POINT ( 'NONE',  ( 3.680118525130245732, -2.494084732383344605, -0.3507732604232533524 ) ) ;
#1635=CARTESIAN_POINT ( 'NONE',  ( -1.654252653721913102, -3.663718938583024443, -0.01223254789874440342 ) ) ;
#1641=( GEOMETRIC_REPRESENTATION_CONTEXT ( 3 ) GLOBAL_UNCERTAINTY_ASSIGNED_CONTEXT ( ( #12772 ) ) GLOBAL_UNIT_ASSIGNED_CONTEXT ( ( #9225, #2846, #1518 ) ) REPRESENTATION_CONTEXT ( 'NONE', 'WORKASPACE' ) );
#1646=CARTESIAN_POINT ( 'NONE',  ( 0.1750025118121568690, 4.719839900820621104, -3.469254087858248070 ) ) ;
#1648=VECTOR ( 'NONE', #2392, 1000.000000000000000 ) ;
#1651=FACE_BOUND ( 'NONE', #10444, .T. ) ;
#1657=CARTESIAN_POINT ( 'NONE',  ( -4.198928548860774157, 0.8158838809860065044, -3.526471437616918170 ) ) ;
#1671=CARTESIAN_POINT ( 'NONE',  ( 4.000000000000000000, 2.309401076758497151, -5.000000000000000000 ) ) ;
#1683=CARTESIAN_POINT ( 'NONE',  ( 0.000000000000000000, 0.000000000000000000, 0.000000000000000000 ) ) ;
#1706=DIRECTION ( 'NONE',  ( 1.000000000000000000, 0.000000000000000000, 0.000000000000000000 ) ) ;
#1798=EDGE_CURVE ( 'NONE', #6723, #8744, #10669, .T. ) ;
#1799=CARTESIAN_POINT ( 'NONE',  ( -0.5276280594146446346, 4.314175951381965746, -3.320322319201721495 ) ) ;
#1867=( NAMED_UNIT ( * ) PLANE_ANGLE_UNIT ( ) SI_UNIT ( $, .RADIAN. ) );
#1869=CARTESIAN_POINT ( 'NONE',  ( 4.000000000000000000, -2.511475576507276042, -3.469253905236643565 ) ) ;
#1883=CARTESIAN_POINT ( 'NONE',  ( -4.211140560182196957, 2.431303136016537803, -3.745885042887433514 ) ) ;
#1912=UNCERTAINTY_MEASURE_WITH_UNIT (LENGTH_MEASURE( 1.000000000000000082E-05 ), #12564, 'distance_accuracy_value', 'NONE');
#1940=DIRECTION ( 'NONE',  ( -0.000000000000000000, 0.000000000000000000, -1.000000000000000000 ) ) ;
#1954=CARTESIAN_POINT ( 'NONE',  ( -4.197393957002303999, -0.8151795401431414234, -3.503767560748935139 ) ) ;
#1962=CARTESIAN_POINT ( 'NONE',  ( -4.000000000000000000, 1.677772373332757194, -3.535253723897187506 ) ) ;
#1964=VERTEX_POINT ( 'NONE', #2095 ) ;
#1969=CARTESIAN_POINT ( 'NONE',  ( -4.101948962586059011, 2.368261337751163875, -3.681124513963739187 ) ) ;
#1974=ORIENTED_EDGE ( 'NONE', *, *, #10486, .F. ) ;
#1985=B_SPLINE_CURVE_WITH_KNOTS ( 'NONE', 3,
 ( #6018, #6839, #213, #478, #3054, #7394 ),
 .UNSPECIFIED., .F., .F.,
 ( 4, 2, 4 ),
 ( -3.640115492407174633E-06, 0.0002066546034003413743, 0.0004169493222930899571 ),
 .UNSPECIFIED. ) ;
#1991=CARTESIAN_POINT ( 'NONE',  ( 2.805705207896068476, -3.226868319750173075, -3.503898532754370354 ) ) ;
#2006=VERTEX_POINT ( 'NONE', #10647 ) ;
#2009=CARTESIAN_POINT ( 'NONE',  ( -2.500000000000000444, 3.061616997868383634E-16, -5.000000000000000888 ) ) ;
#2033=ADVANCED_FACE ( 'NONE', ( #9479 ), #9743, .F. ) ;
#2043=AXIS2_PLACEMENT_3D ( 'NONE', #5978, #13653, #10473 ) ;
#2066=ADVANCED_FACE ( 'NONE', ( #3968 ), #4040, .F. ) ;
#2071=B_SPLINE_CURVE_WITH_KNOTS ( 'NONE', 3,
 ( #9165, #4753, #8906, #4416, #12235, #14257, #8832, #5565 ),
 .UNSPECIFIED., .F., .F.,
 ( 4, 2, 2, 4 ),
 ( 2.465131517075058656E-07, 0.001183067374689851080, 0.001774477805458923299, 0.002365888236227995517 ),
 .UNSPECIFIED. ) ;
#2094=FACE_OUTER_BOUND ( 'NONE', #692, .T. ) ;
#2095=CARTESIAN_POINT ( 'NONE',  ( -2.100000000000000089, 2.571758278209441957E-16, -0.2800830152838844622 ) ) ;
#2118=ORIENTED_EDGE ( 'NONE', *, *, #10938, .T. ) ;
#2126=B_SPLINE_CURVE_WITH_KNOTS ( 'NONE', 3,
 ( #8464, #10582, #12826, #10510, #3980, #9571, #13979, #4051 ),
 .UNSPECIFIED., .F., .F.,
 ( 4, 2, 2, 4 ),
 ( 0.000000000000000000, 0.002450665683189818828, 0.003675998524784728459, 0.004901331366379638524 ),
 .UNSPECIFIED. ) ;
#2133=ORIENTED_EDGE ( 'NONE', *, *, #10960, .F. ) ;
#2138=LINE ( 'NONE', #952, #9182 ) ;
#2145=AXIS2_PLACEMENT_3D ( 'NONE', #591, #5989, #12873 ) ;
#2231=ORIENTED_EDGE ( 'NONE', *, *, #7973, .T. ) ;
#2232=STYLED_ITEM('',(#14417),#8769);
#2299=CARTESIAN_POINT ( 'NONE',  ( 4.000000000000000000, -1.942223658245635809, -0.3516579909967643691 ) ) ;
#2300=EDGE_CURVE ( 'NONE', #14086, #931, #8673, .T. ) ;
#2307=CARTESIAN_POINT ( 'NONE',  ( 4.000000000000000000, 2.309401076758497151, -3.433295621305379353 ) ) ;
#2335=DIRECTION ( 'NONE',  ( -0.000000000000000000, -0.000000000000000000, 1.000000000000000000 ) ) ;
#2348=ORIENTED_EDGE ( 'NONE', *, *, #1480, .F. ) ;
#2351=VERTEX_POINT ( 'NONE', #11355 ) ;
#2358=( BOUNDED_SURFACE ( )  B_SPLINE_SURFACE ( 3, 2, ( 
 ( #5514, #9869, #4431 ),
 ( #14277, #6741, #13121 ),
 ( #5716, #12466, #4717 ),
 ( #12539, #1564, #9127 ),
 ( #1491, #9352, #2531 ),
 ( #6810, #8101, #11520 ) ),
 .UNSPECIFIED., .F., .F., .T. ) 
 B_SPLINE_SURFACE_WITH_KNOTS ( ( 4, 2, 4 ),
 ( 3, 3 ),
 ( 0.02032853247518126918, 0.02278863295364821906, 0.02524873343211516893 ),
 ( 0.000000000000000000, 1.000000000000000000 ),
 .UNSPECIFIED. ) 
 GEOMETRIC_REPRESENTATION_ITEM ( )  RATIONAL_B_SPLINE_SURFACE ( (
 ( 1.000000000000000000, 0.8047781615896838492, 1.000000000000000000),
 ( 1.000000000000000000, 0.8123767586288186404, 1.000000000000000000),
 ( 1.000000000000000000, 0.8190662415565814758, 1.000000000000000000),
 ( 1.000000000000000000, 0.8192361015667604107, 1.000000000000000000),
 ( 1.000000000000000000, 0.8126135807104967190, 1.000000000000000000),
 ( 1.000000000000000000, 0.8047712338318580017, 1.000000000000000000) ) ) 
 REPRESENTATION_ITEM ( '' )  SURFACE ( )  );
#2363=AXIS2_PLACEMENT_3D ( 'NONE', #9130, #4720, #4646 ) ;
#2392=DIRECTION ( 'NONE',  ( 0.000000000000000000, 0.000000000000000000, 1.000000000000000000 ) ) ;
#2395=DIRECTION ( 'NONE',  ( 0.000000000000000000, -1.000000000000000000, 0.000000000000000000 ) ) ;
#2397=VERTEX_POINT ( 'NONE', #13376 ) ;
#2406=DIRECTION ( 'NONE',  ( -0.000000000000000000, -0.000000000000000000, 1.000000000000000000 ) ) ;
#2416=ADVANCED_FACE ( 'NONE', ( #3526 ), #13664, .T. ) ;
#2451=ORIENTED_EDGE ( 'NONE', *, *, #1391, .F. ) ;
#2453=CARTESIAN_POINT ( 'NONE',  ( 4.140404888673277384, 2.228338276487440428, -3.686887068327033390 ) ) ;
#2471=VERTEX_POINT ( 'NONE', #7770 ) ;
#2483=ADVANCED_FACE ( 'NONE', ( #10038 ), #9155, .T. ) ;
#2488=VERTEX_POINT ( 'NONE', #5671 ) ;
#2501=B_SPLINE_CURVE_WITH_KNOTS ( 'NONE', 3,
 ( #11126, #1161, #5398, #14229, #8939, #10036 ),
 .UNSPECIFIED., .F., .F.,
 ( 4, 2, 4 ),
 ( 0.000000000000000000, 0.0002095117440864783663, 0.0004190234881729567326 ),
 .UNSPECIFIED. ) ;
#2531=CARTESIAN_POINT ( 'NONE',  ( -0.6810597143197697489, -4.461075778259609770, -3.598441714920717516 ) ) ;
#2556=PRESENTATION_STYLE_ASSIGNMENT (( #490 ) ) ;
#2567=ORIENTED_EDGE ( 'NONE', *, *, #5765, .F. ) ;
#2596=CARTESIAN_POINT ( 'NONE',  ( -1.828356344711647319, -3.563200125723192002, -1.076197711133951296E-14 ) ) ;
#2608=DIRECTION ( 'NONE',  ( 0.8660254037844374864, -0.5000000000000018874, 0.000000000000000000 ) ) ;
#2640=ORIENTED_EDGE ( 'NONE', *, *, #1480, .T. ) ;
#2646=CARTESIAN_POINT ( 'NONE',  ( 0.000000000000000000, 0.000000000000000000, -5.000000000000000888 ) ) ;
#2648=DIRECTION ( 'NONE',  ( 0.000000000000000000, 0.000000000000000000, 1.000000000000000000 ) ) ;
#2652=DIRECTION ( 'NONE',  ( -0.8191520442889902442, 0.000000000000000000, -0.5735764363510482688 ) ) ;
#2670=EDGE_CURVE ( 'NONE', #4036, #2471, #4699, .T. ) ;
#2673=CARTESIAN_POINT ( 'NONE',  ( -2.687328764639638656, 3.067272167851286202, -0.05923475698270370959 ) ) ;
#2677=VERTEX_POINT ( 'NONE', #12412 ) ;
#2683=CARTESIAN_POINT ( 'NONE',  ( 4.211140560182196957, -2.431303136016555122, -3.745885042887436622 ) ) ;
#2685=ADVANCED_FACE ( 'NONE', ( #5816 ), #7045, .F. ) ;
#2699=FILL_AREA_STYLE_COLOUR ( '', #13726 ) ;
#2710=VERTEX_POINT ( 'NONE', #5888 ) ;
#2717=AXIS2_PLACEMENT_3D ( 'NONE', #1683, #4894, #13871 ) ;
#2723=EDGE_CURVE ( 'NONE', #2940, #13395, #1386, .T. ) ;
#2733=ORIENTED_EDGE ( 'NONE', *, *, #9631, .T. ) ;
#2751=CARTESIAN_POINT ( 'NONE',  ( -3.455068668934486276, 2.624017327439035707, -3.316620875263955437 ) ) ;
#2760=CARTESIAN_POINT ( 'NONE',  ( -0.3461262719736137305, 4.658553426539289610, -3.671615880910373608 ) ) ;
#2761=ORIENTED_EDGE ( 'NONE', *, *, #1527, .F. ) ;
#2770=SHAPE_REPRESENTATION_RELATIONSHIP ( 'NONE' , 'NONE' ,  #9307, #12151 ) ;
#2775=CARTESIAN_POINT ( 'NONE',  ( -0.6666666666666651864, 4.233901974057260098, -3.300726591567081147 ) ) ;
#2776=ORIENTED_EDGE ( 'NONE', *, *, #10321, .T. ) ;
#2788=CARTESIAN_POINT ( 'NONE',  ( 4.197393957002303999, 7.772902908466098641E-14, -3.503767560748929810 ) ) ;
#2827=CARTESIAN_POINT ( 'NONE',  ( 3.999999999999999112, 1.941961291383486277, -0.3515519931180248192 ) ) ;
#2839=FACE_OUTER_BOUND ( 'NONE', #4330, .T. ) ;
#2846=( NAMED_UNIT ( * ) PLANE_ANGLE_UNIT ( ) SI_UNIT ( $, .RADIAN. ) );
#2857=CARTESIAN_POINT ( 'NONE',  ( 2.855764796983346177, -2.970025579236428737, -0.09382832055446485575 ) ) ;
#2864=UNCERTAINTY_MEASURE_WITH_UNIT (LENGTH_MEASURE( 1.000000000000000082E-05 ), #10947, 'distance_accuracy_value', 'NONE');
#2874=CARTESIAN_POINT ( 'NONE',  ( -4.000000000000000000, -2.309401076758512694, -3.433295621305382461 ) ) ;
#2879=DIRECTION ( 'NONE',  ( -1.000000000000000000, 0.000000000000000000, 0.000000000000000000 ) ) ;
#2886=DIRECTION ( 'NONE',  ( 1.000000000000000000, 0.000000000000000000, 0.000000000000000000 ) ) ;
#2898=CARTESIAN_POINT ( 'NONE',  ( 4.000000000000000000, 0.7924765000094659007, -0.05906175389889852662 ) ) ;
#2923=B_SPLINE_CURVE_WITH_KNOTS ( 'NONE', 3,
 ( #12118, #4603, #6779, #7644, #12081, #4398 ),
 .UNSPECIFIED., .F., .F.,
 ( 4, 2, 4 ),
 ( 0.002365888236228001588, 0.003551327329835089319, 0.004736766423442177049 ),
 .UNSPECIFIED. ) ;
#2940=VERTEX_POINT ( 'NONE', #14280 ) ;
#2977=CARTESIAN_POINT ( 'NONE',  ( 4.000000000000000000, 0.3987449864460005378, -0.01220643443059817035 ) ) ;
#2988=CARTESIAN_POINT ( 'NONE',  ( -4.000000000000000000, 0.000000000000000000, 0.000000000000000000 ) ) ;
#3005=ORIENTED_EDGE ( 'NONE', *, *, #802, .T. ) ;
#3035=ORIENTED_EDGE ( 'NONE', *, *, #4391, .T. ) ;
#3045=CARTESIAN_POINT ( 'NONE',  ( 1.999999999999998224, -3.464101615137772594, -3.142992957459239012 ) ) ;
#3046=CARTESIAN_POINT ( 'NONE',  ( 4.000000000000000888, -0.8578082829538523635, -3.433262215449808696 ) ) ;
#3054=CARTESIAN_POINT ( 'NONE',  ( 1.567478505476134803E-15, 4.618802153517012954, -3.504269196027872457 ) ) ;
#3067=VECTOR ( 'NONE', #5517, 1000.000000000000227 ) ;
#3079=ORIENTED_EDGE ( 'NONE', *, *, #4278, .F. ) ;
#3096=CONICAL_SURFACE ( 'NONE', #5569, 2.059999999999998721, 0.9599310885968738161 ) ;
#3102=CARTESIAN_POINT ( 'NONE',  ( 0.6937372685066666156, -4.453844082567737672, -3.610536846335894445 ) ) ;
#3105=ORIENTED_EDGE ( 'NONE', *, *, #14237, .F. ) ;
#3116=EDGE_CURVE ( 'NONE', #4974, #1964, #447, .T. ) ;
#3145=ADVANCED_FACE ( 'NONE', ( #7028 ), #11240, .F. ) ;
#3166=CIRCLE ( 'NONE', #11714, 2.499999999999999556 ) ;
#3214=FACE_OUTER_BOUND ( 'NONE', #5311, .T. ) ;
#3216=CARTESIAN_POINT ( 'NONE',  ( -4.000000000000000000, 2.471528634177585282, -3.686887442155186712 ) ) ;
#3218=ORIENTED_EDGE ( 'NONE', *, *, #1527, .T. ) ;
#3221=ORIENTED_EDGE ( 'NONE', *, *, #11547, .F. ) ;
#3284=CARTESIAN_POINT ( 'NONE',  ( -2.000000000000006661, 3.464101615137750834, 0.000000000000000000 ) ) ;
#3305=FACE_OUTER_BOUND ( 'NONE', #3839, .T. ) ;
#3312=VERTEX_POINT ( 'NONE', #6081 ) ;
#3325=EDGE_CURVE ( 'NONE', #2471, #14086, #2126, .T. ) ;
#3328=ADVANCED_FACE ( 'NONE', ( #11814 ), #12731, .F. ) ;
#3348=CARTESIAN_POINT ( 'NONE',  ( -4.000000000000000000, 0.000000000000000000, 0.000000000000000000 ) ) ;
#3360=CARTESIAN_POINT ( 'NONE',  ( -0.6507732100473471171, 4.243078065514775510, -0.2236248678334823436 ) ) ;
#3389=CARTESIAN_POINT ( 'NONE',  ( -4.154094228333820915, -2.398367420967594921, -3.721909803043257803 ) ) ;
#3418=APPLICATION_CONTEXT ( 'automotive_design' ) ;
#3419=DIRECTION ( 'NONE',  ( 1.000000000000000000, 0.000000000000000000, 0.000000000000000000 ) ) ;
#3455=CARTESIAN_POINT ( 'NONE',  ( 4.000000000000000000, 2.512223110932545023, -3.469391141908803711 ) ) ;
#3476=CARTESIAN_POINT ( 'NONE',  ( 1.243802165048773611, -3.900692638707475624, -3.223146290109810241 ) ) ;
#3481=CARTESIAN_POINT ( 'NONE',  ( 1.390230914382191596, 4.043987460488659202, -3.502507215260488582 ) ) ;
#3502=ORIENTED_EDGE ( 'NONE', *, *, #13999, .F. ) ;
#3511=CARTESIAN_POINT ( 'NONE',  ( -2.500000000000000444, 3.061616997868383634E-16, -25.03750572909317285 ) ) ;
#3526=FACE_OUTER_BOUND ( 'NONE', #12309, .T. ) ;
#3534=ORIENTED_EDGE ( 'NONE', *, *, #8685, .T. ) ;
#3552=CARTESIAN_POINT ( 'NONE',  ( 4.175002511812151873, 2.208363329454889445, -3.469254087858244073 ) ) ;
#3570=DIRECTION ( 'NONE',  ( 0.000000000000000000, 0.000000000000000000, -1.000000000000000000 ) ) ;
#3592=FACE_OUTER_BOUND ( 'NONE', #11896, .T. ) ;
#3598=CARTESIAN_POINT ( 'NONE',  ( -2.000000000000006661, 3.464101615137750834, 0.000000000000000000 ) ) ;
#3612=ORIENTED_EDGE ( 'NONE', *, *, #13817, .F. ) ;
#3615=CARTESIAN_POINT ( 'NONE',  ( 1.287237434362044075, 3.875615274277557809, -3.430618716626812059 ) ) ;
#3623=EDGE_CURVE ( 'NONE', #4356, #3798, #9295, .T. ) ;
#3647=AXIS2_PLACEMENT_3D ( 'NONE', #7773, #7708, #13725 ) ;
#3654=ORIENTED_EDGE ( 'NONE', *, *, #7997, .F. ) ;
#3685=PRODUCT_DEFINITION_SHAPE ( 'NONE', 'NONE',  #10925 ) ;
#3707=AXIS2_PLACEMENT_3D ( 'NONE', #602, #11876, #2886 ) ;
#3721=DIRECTION ( 'NONE',  ( -0.000000000000000000, -0.000000000000000000, 1.000000000000000000 ) ) ;
#3753=EDGE_CURVE ( 'NONE', #8807, #2351, #8878, .T. ) ;
#3777=CARTESIAN_POINT ( 'NONE',  ( 4.024499207728847949, -2.323545700935699454, -3.572172305156873673 ) ) ;
#3793=B_SPLINE_CURVE_WITH_KNOTS ( 'NONE', 3,
 ( #13799, #3800, #6121, #4087, #8510, #13947, #4023, #10398 ),
 .UNSPECIFIED., .F., .F.,
 ( 4, 2, 2, 4 ),
 ( 7.780516681398759253E-20, 0.002450665683189819696, 0.003675998524784729327, 0.004901331366379639391 ),
 .UNSPECIFIED. ) ;
#3798=VERTEX_POINT ( 'NONE', #11336 ) ;
#3800=CARTESIAN_POINT ( 'NONE',  ( 0.6920835326022565237, 4.454600218803884459, -3.597382984111579862 ) ) ;
#3821=CARTESIAN_POINT ( 'NONE',  ( -0.6448876103708541807, -4.246476118072358474, -0.2256878752776773356 ) ) ;
#3839=EDGE_LOOP ( 'NONE', ( #12883, #2733, #2776, #4531, #6437, #13295, #2231 ) ) ;
#3843=CARTESIAN_POINT ( 'NONE',  ( -0.6937372685066653943, 4.453844082567723461, -3.610536846335889116 ) ) ;
#3852=SURFACE_SIDE_STYLE ('',( #12488 ) ) ;
#3859=ORIENTED_EDGE ( 'NONE', *, *, #12953, .F. ) ;
#3886=CARTESIAN_POINT ( 'NONE',  ( 1.655952806101427033, -3.662737355149048302, -1.182683869819604841E-14 ) ) ;
#3896=DIRECTION ( 'NONE',  ( -0.000000000000000000, -0.000000000000000000, 1.000000000000000000 ) ) ;
#3909=DIRECTION ( 'NONE',  ( -0.5000000000000019984, -0.8660254037844375974, 0.000000000000000000 ) ) ;
#3912=CARTESIAN_POINT ( 'NONE',  ( 4.000000000000000888, 1.563622288139206118, -0.2253451193528334950 ) ) ;
#3920=VERTEX_POINT ( 'NONE', #4004 ) ;
#3921=CARTESIAN_POINT ( 'NONE',  ( -4.207491450040567571, 2.029819825146470524, -3.671670828759566074 ) ) ;
#3936=ORIENTED_EDGE ( 'NONE', *, *, #7699, .F. ) ;
#3944=ORIENTED_EDGE ( 'NONE', *, *, #9760, .T. ) ;
#3950=CARTESIAN_POINT ( 'NONE',  ( 1.567478505476134606E-15, 4.618802153517012066, -5.000000000000000000 ) ) ;
#3968=FACE_OUTER_BOUND ( 'NONE', #11961, .T. ) ;
#3975=LINE ( 'NONE', #10734, #596 ) ;
#3980=CARTESIAN_POINT ( 'NONE',  ( -2.804994570502171047, -3.229033611042465335, -3.526374918436838701 ) ) ;
#3983=CARTESIAN_POINT ( 'NONE',  ( -0.6640947660597427138, 4.471078309994878985, -3.602146406945963442 ) ) ;
#3995=ORIENTED_EDGE ( 'NONE', *, *, #8942, .F. ) ;
#4004=CARTESIAN_POINT ( 'NONE',  ( -2.499999999999999556, 3.061616997868382648E-16, 3.469446951953614189E-15 ) ) ;
#4017=ORIENTED_EDGE ( 'NONE', *, *, #13817, .T. ) ;
#4022=DIRECTION ( 'NONE',  ( 0.000000000000000000, 0.000000000000000000, 1.000000000000000000 ) ) ;
#4023=CARTESIAN_POINT ( 'NONE',  ( 3.861362476283255685, 2.629030857715988656, -3.671615880910370500 ) ) ;
#4027=ADVANCED_FACE ( 'NONE', ( #6465 ), #12027, .F. ) ;
#4030=ORIENTED_EDGE ( 'NONE', *, *, #12798, .T. ) ;
#4036=VERTEX_POINT ( 'NONE', #7755 ) ;
#4040=CYLINDRICAL_SURFACE ( 'NONE', #5630, 2.500000000000000444 ) ;
#4051=CARTESIAN_POINT ( 'NONE',  ( -4.211140560182196957, -2.431303136016552013, -3.745885042887436178 ) ) ;
#4055=CARTESIAN_POINT ( 'NONE',  ( 4.000000000000000000, 0.1981133338132474442, 2.382280164152719704E-17 ) ) ;
#4059=DIRECTION ( 'NONE',  ( -0.000000000000000000, -0.000000000000000000, 1.000000000000000000 ) ) ;
#4061=AXIS2_PLACEMENT_3D ( 'NONE', #11749, #628, #9503 ) ;
#4066=CARTESIAN_POINT ( 'NONE',  ( -4.000000000000000000, 0.1981133338132459731, 2.096406544454392723E-17 ) ) ;
#4082=CARTESIAN_POINT ( 'NONE',  ( 1.734723475976807094E-15, 4.618802153517012954, -0.4999999999999995559 ) ) ;
#4087=CARTESIAN_POINT ( 'NONE',  ( 2.449848172108560096, 3.432307619358740514, -3.503702292528905637 ) ) ;
#4098=AXIS2_PLACEMENT_3D ( 'NONE', #7985, #10255, #9161 ) ;
#4106=ADVANCED_FACE ( 'NONE', ( #5446, #3214 ), #14284, .F. ) ;
#4126=EDGE_CURVE ( 'NONE', #13395, #8791, #10417, .T. ) ;
#4129=CARTESIAN_POINT ( 'NONE',  ( 4.000000000000000000, -1.677850389431204459, -3.535268758346977513 ) ) ;
#4148=CARTESIAN_POINT ( 'NONE',  ( -4.204114297095464359, 1.660363174096617156, -3.602136431857887011 ) ) ;
#4171=EDGE_CURVE ( 'NONE', #4511, #10102, #11127, .T. ) ;
#4186=CARTESIAN_POINT ( 'NONE',  ( -3.999999999999999112, -2.309401076758512694, -3.504269196027871125 ) ) ;
#4191=EDGE_CURVE ( 'NONE', #32, #10991, #1345, .T. ) ;
#4198=CARTESIAN_POINT ( 'NONE',  ( 4.211140560182196957, -2.431303136016555122, -3.745885042887436622 ) ) ;
#4201=DIRECTION ( 'NONE',  ( -1.000000000000000000, 0.000000000000000000, 0.000000000000000000 ) ) ;
#4231=CARTESIAN_POINT ( 'NONE',  ( -4.024497503033714452, 2.323544716729487813, -3.572167766733750582 ) ) ;
#4258=ADVANCED_FACE ( 'NONE', ( #7094 ), #1241, .F. ) ;
#4270=CARTESIAN_POINT ( 'NONE',  ( 2.000000000000008882, 3.464101615137749945, 0.000000000000000000 ) ) ;
#4278=EDGE_CURVE ( 'NONE', #5507, #10102, #8519, .T. ) ;
#4285=DIRECTION ( 'NONE',  ( 0.000000000000000000, 0.000000000000000000, 1.000000000000000000 ) ) ;
#4300=EDGE_LOOP ( 'NONE', ( #9971, #55, #12916, #12028, #5157 ) ) ;
#4328=CIRCLE ( 'NONE', #4098, 2.100000000000000089 ) ;
#4330=EDGE_LOOP ( 'NONE', ( #7525, #6508, #5557 ) ) ;
#4331=DIRECTION ( 'NONE',  ( 1.000000000000000000, 0.000000000000000000, 0.000000000000000000 ) ) ;
#4356=VERTEX_POINT ( 'NONE', #10661 ) ;
#4378=ORIENTED_EDGE ( 'NONE', *, *, #11183, .T. ) ;
#4391=EDGE_CURVE ( 'NONE', #2488, #2710, #7388, .T. ) ;
#4398=CARTESIAN_POINT ( 'NONE',  ( -4.000000000000000000, -2.309401076758515803, -0.4999999999999995559 ) ) ;
#4416=CARTESIAN_POINT ( 'NONE',  ( 1.144235203016666258, 3.958177651039090250, -0.09382832055445661235 ) ) ;
#4421=AXIS2_PLACEMENT_3D ( 'NONE', #389, #5866, #4859 ) ;
#4425=CARTESIAN_POINT ( 'NONE',  ( -4.000000000000000000, -1.942223658245633811, -0.3516579909967644246 ) ) ;
#4431=CARTESIAN_POINT ( 'NONE',  ( -4.235886605889389145, -2.417314728048544303, -3.751161874094020909 ) ) ;
#4440=CARTESIAN_POINT ( 'NONE',  ( -4.000000000000000000, 0.8576368993457507139, -3.433240632782198709 ) ) ;
#4471=DIRECTION ( 'NONE',  ( -1.000000000000000000, 0.000000000000000000, 0.000000000000000000 ) ) ;
#4480=CARTESIAN_POINT ( 'NONE',  ( -4.000000000000000000, -2.309401076758512694, -3.433295621305382461 ) ) ;
#4497=CARTESIAN_POINT ( 'NONE',  ( 1.257172072275274388, -3.892973519170983110, -3.433252694550781303 ) ) ;
#4511=VERTEX_POINT ( 'NONE', #4270 ) ;
#4514=CARTESIAN_POINT ( 'NONE',  ( -4.211140560182196957, 2.431303136016537803, -3.745885042887433514 ) ) ;
#4517=ORIENTED_EDGE ( 'NONE', *, *, #3753, .T. ) ;
#4531=ORIENTED_EDGE ( 'NONE', *, *, #1798, .F. ) ;
#4543=DIRECTION ( 'NONE',  ( 1.000000000000000000, 0.000000000000000000, 0.000000000000000000 ) ) ;
#4601=CARTESIAN_POINT ( 'NONE',  ( 4.000000000000003553, -2.309401076758513138, -3.504271511727127031 ) ) ;
#4603=CARTESIAN_POINT ( 'NONE',  ( -2.344047193898593395, -3.265465875126480455, -1.054683074273691752E-14 ) ) ;
#4607=CARTESIAN_POINT ( 'NONE',  ( 4.000000000000000888, 0.8228435280416209752, -3.430609588141487976 ) ) ;
#4608=AXIS2_PLACEMENT_3D ( 'NONE', #9810, #12262, #6539 ) ;
#4609=PLANE ( 'NONE',  #8805 ) ;
#4634=CARTESIAN_POINT ( 'NONE',  ( 4.236525694536557474, -2.416953475386482530, -3.751298745799839462 ) ) ;
#4636=ORIENTED_EDGE ( 'NONE', *, *, #10938, .F. ) ;
#4639=EDGE_CURVE ( 'NONE', #2397, #11069, #10201, .T. ) ;
#4646=DIRECTION ( 'NONE',  ( 1.000000000000000000, 0.000000000000000000, 0.000000000000000000 ) ) ;
#4650=CARTESIAN_POINT ( 'NONE',  ( 4.197393957002303999, -0.4069871074557456780, -3.503767560748925813 ) ) ;
#4661=ORIENTED_EDGE ( 'NONE', *, *, #7816, .T. ) ;
#4672=ORIENTED_EDGE ( 'NONE', *, *, #13115, .F. ) ;
#4674=ADVANCED_FACE ( 'NONE', ( #11508 ), #376, .T. ) ;
#4686=AXIS2_PLACEMENT_3D ( 'NONE', #9244, #579, #8364 ) ;
#4691=AXIS2_PLACEMENT_3D ( 'NONE', #5807, #2335, #10232 ) ;
#4699=B_SPLINE_CURVE_WITH_KNOTS ( 'NONE', 3,
 ( #9224, #6829, #4952, #1516, #13711, #6029 ),
 .UNSPECIFIED., .F., .F.,
 ( 4, 2, 4 ),
 ( 0.000000000000000000, 0.0002095117440864791795, 0.0004190234881729583589 ),
 .UNSPECIFIED. ) ;
#4712=CARTESIAN_POINT ( 'NONE',  ( 3.522875095019493141, -2.820352903225631369, -3.598441714920572299 ) ) ;
#4717=CARTESIAN_POINT ( 'NONE',  ( -2.836893136758495970, -3.208949435745868328, -3.505054077164885484 ) ) ;
#4720=DIRECTION ( 'NONE',  ( -0.000000000000000000, -0.000000000000000000, 1.000000000000000000 ) ) ;
#4753=CARTESIAN_POINT ( 'NONE',  ( 0.3198814748697593746, 4.434118497892183264, -0.3507732604232499107 ) ) ;
#4781=CARTESIAN_POINT ( 'NONE',  ( 4.000000000000000000, -2.309401076758514915, -5.000000000000000000 ) ) ;
#4807=CARTESIAN_POINT ( 'NONE',  ( 4.203833317240879275, 1.627343821129582979, -3.597273115243889929 ) ) ;
#4813=ORIENTED_EDGE ( 'NONE', *, *, #4126, .F. ) ;
#4830=FACE_OUTER_BOUND ( 'NONE', #6116, .T. ) ;
#4859=DIRECTION ( 'NONE',  ( 1.000000000000000000, 0.000000000000000000, 0.000000000000000000 ) ) ;
#4860=CARTESIAN_POINT ( 'NONE',  ( -3.680118525130244400, 2.494084732383327285, -0.3507732604232449702 ) ) ;
#4894=DIRECTION ( 'NONE',  ( -0.000000000000000000, 0.000000000000000000, -1.000000000000000000 ) ) ;
#4928=CARTESIAN_POINT ( 'NONE',  ( 3.472371940585993855, 2.614027278893175321, -3.320322319201766792 ) ) ;
#4952=CARTESIAN_POINT ( 'NONE',  ( -1.149515148933674504E-15, -4.647091401871393579, -3.572172305156879890 ) ) ;
#4953=B_SPLINE_CURVE_WITH_KNOTS ( 'NONE', 3,
 ( #14241, #13238, #1991, #5413, #8741, #3102, #11884, #12145 ),
 .UNSPECIFIED., .F., .F.,
 ( 4, 2, 2, 4 ),
 ( 0.000000000000000000, 0.002450665683189819262, 0.003675998524784728893, 0.004901331366379639391 ),
 .UNSPECIFIED. ) ;
#4974=VERTEX_POINT ( 'NONE', #9913 ) ;
#5004=CARTESIAN_POINT ( 'NONE',  ( 4.000000000000000000, 0.000000000000000000, 0.000000000000000000 ) ) ;
#5023=FILL_AREA_STYLE ('',( #2699 ) ) ;
#5060=TOROIDAL_SURFACE ( 'NONE', #5499, 5.384454397937118664, 0.5155456020628804703 ) ;
#5077=DIRECTION ( 'NONE',  ( 1.000000000000000000, 0.000000000000000000, 0.000000000000000000 ) ) ;
#5106=DIRECTION ( 'NONE',  ( 0.000000000000000000, 0.000000000000000000, 1.000000000000000000 ) ) ;
#5143=VECTOR ( 'NONE', #7911, 1000.000000000000000 ) ;
#5157=ORIENTED_EDGE ( 'NONE', *, *, #12073, .T. ) ;
#5171=ORIENTED_EDGE ( 'NONE', *, *, #7820, .F. ) ;
#5181=DIRECTION ( 'NONE',  ( -1.000000000000000000, 0.000000000000000000, 0.000000000000000000 ) ) ;
#5187=EDGE_CURVE ( 'NONE', #3312, #8807, #12729, .T. ) ;
#5216=ADVANCED_FACE ( 'NONE', ( #3592 ), #4609, .T. ) ;
#5217=ORIENTED_EDGE ( 'NONE', *, *, #7973, .F. ) ;
#5220=CARTESIAN_POINT ( 'NONE',  ( 4.211399257449709665, -2.459727064652517114, -3.751161691472417736 ) ) ;
#5236=FACE_OUTER_BOUND ( 'NONE', #5976, .T. ) ;
#5244=ORIENTED_EDGE ( 'NONE', *, *, #6939, .T. ) ;
#5268=CIRCLE ( 'NONE', #13351, 2.500000000000000444 ) ;
#5276=CIRCLE ( 'NONE', #2717, 4.000000000000000000 ) ;
#5277=ORIENTED_EDGE ( 'NONE', *, *, #802, .F. ) ;
#5287=ORIENTED_EDGE ( 'NONE', *, *, #12821, .F. ) ;
#5289=VERTEX_POINT ( 'NONE', #10774 ) ;
#5291=AXIS2_PLACEMENT_3D ( 'NONE', #6950, #1279, #3419 ) ;
#5304=CARTESIAN_POINT ( 'NONE',  ( -5.384454397937118664, 6.594054843588581554E-16, -4.484454397937119197 ) ) ;
#5310=CARTESIAN_POINT ( 'NONE',  ( -4.000000000000000000, 0.3987449864459974846, -0.01220643443059782861 ) ) ;
#5311=EDGE_LOOP ( 'NONE', ( #13955, #7155, #9604, #3995, #14191, #6739 ) ) ;
#5315=CARTESIAN_POINT ( 'NONE',  ( -4.000000000000000000, 0.8730739991738342143, -3.223134629628428893 ) ) ;
#5317=ORIENTED_EDGE ( 'NONE', *, *, #4278, .T. ) ;
#5374=EDGE_LOOP ( 'NONE', ( #664, #6817 ) ) ;
#5377=DIRECTION ( 'NONE',  ( 1.000000000000000000, 0.000000000000000000, 0.000000000000000000 ) ) ;
#5383=CARTESIAN_POINT ( 'NONE',  ( -1.655952806101422814, 3.662737355149034979, -7.623296525288699970E-18 ) ) ;
#5398=CARTESIAN_POINT ( 'NONE',  ( 4.024499207728848837, 2.323545700935681246, -3.572172305156870564 ) ) ;
#5413=CARTESIAN_POINT ( 'NONE',  ( 1.747541505913279281, -3.837784562140273081, -3.503702292528912299 ) ) ;
#5434=CARTESIAN_POINT ( 'NONE',  ( -0.1404048886732797152, -4.699864953788083888, -3.686887068327043160 ) ) ;
#5439=ADVANCED_FACE ( 'NONE', ( #3305 ), #7588, .T. ) ;
#5446=FACE_BOUND ( 'NONE', #14080, .T. ) ;
#5499=AXIS2_PLACEMENT_3D ( 'NONE', #10820, #7537, #5377 ) ;
#5500=ORIENTED_EDGE ( 'NONE', *, *, #11764, .F. ) ;
#5507=VERTEX_POINT ( 'NONE', #745 ) ;
#5513=VECTOR ( 'NONE', #6080, 1000.000000000000000 ) ;
#5514=CARTESIAN_POINT ( 'NONE',  ( -4.175002511812151873, -2.208363329454905877, -3.469254087858246738 ) ) ;
#5517=DIRECTION ( 'NONE',  ( 0.9396926207859138680, 1.150791560227856926E-16, -0.3420201433256536139 ) ) ;
#5535=DIRECTION ( 'NONE',  ( -0.000000000000000000, -0.000000000000000000, 1.000000000000000000 ) ) ;
#5542=ORIENTED_EDGE ( 'NONE', *, *, #4639, .F. ) ;
#5557=ORIENTED_EDGE ( 'NONE', *, *, #12073, .F. ) ;
#5565=CARTESIAN_POINT ( 'NONE',  ( 2.000000000000008882, 3.464101615137749945, 0.000000000000000000 ) ) ;
#5569=AXIS2_PLACEMENT_3D ( 'NONE', #11342, #1385, #5896 ) ;
#5630=AXIS2_PLACEMENT_3D ( 'NONE', #676, #3896, #1706 ) ;
#5671=CARTESIAN_POINT ( 'NONE',  ( 2.000000000000005329, -3.464101615137751722, 0.000000000000000000 ) ) ;
#5677=AXIS2_PLACEMENT_3D ( 'NONE', #8145, #13516, #2648 ) ;
#5690=ADVANCED_FACE ( 'NONE', ( #564 ), #10385, .F. ) ;
#5693=EDGE_CURVE ( 'NONE', #5507, #4511, #7348, .T. ) ;
#5714=ORIENTED_EDGE ( 'NONE', *, *, #3116, .T. ) ;
#5716=CARTESIAN_POINT ( 'NONE',  ( -2.756197834950067094, -3.027510591568735254, -3.223146290109809797 ) ) ;
#5738=DIRECTION ( 'NONE',  ( 1.000000000000000000, 0.000000000000000000, 0.000000000000000000 ) ) ;
#5765=EDGE_CURVE ( 'NONE', #1149, #2677, #174, .T. ) ;
#5780=( BOUNDED_SURFACE ( )  B_SPLINE_SURFACE ( 3, 2, ( 
 ( #922, #3216, #6394 ),
 ( #6327, #1962, #4148 ),
 ( #5315, #4440, #6607 ),
 ( #9874, #7542, #9738 ),
 ( #8785, #11914, #13207 ),
 ( #10974, #8710, #14144 ) ),
 .UNSPECIFIED., .F., .F., .F. ) 
 B_SPLINE_SURFACE_WITH_KNOTS ( ( 4, 2, 4 ),
 ( 3, 3 ),
 ( 0.02027752710269158445, 0.02273781595091097299, 0.02519810479913036153 ),
 ( 0.000000000000000000, 1.000000000000000000 ),
 .UNSPECIFIED. ) 
 GEOMETRIC_REPRESENTATION_ITEM ( )  RATIONAL_B_SPLINE_SURFACE ( (
 ( 1.000000000000000000, 0.8047781431712808242, 1.000000000000000000),
 ( 1.000000000000000000, 0.8123773247083928561, 1.000000000000000000),
 ( 1.000000000000000000, 0.8190670192154906326, 1.000000000000000000),
 ( 1.000000000000000000, 0.8192353552912178261, 1.000000000000000000),
 ( 1.000000000000000000, 0.8126132098226825917, 1.000000000000000000),
 ( 1.000000000000000000, 0.8047712465856394770, 1.000000000000000000) ) ) 
 REPRESENTATION_ITEM ( '' )  SURFACE ( )  );
#5806=ORIENTED_EDGE ( 'NONE', *, *, #894, .F. ) ;
#5807=CARTESIAN_POINT ( 'NONE',  ( 0.000000000000000000, 0.000000000000000000, -4.694516984716113228 ) ) ;
#5808=EDGE_LOOP ( 'NONE', ( #10571, #6102, #12268, #3079, #5171 ) ) ;
#5816=FACE_OUTER_BOUND ( 'NONE', #8983, .T. ) ;
#5855=CARTESIAN_POINT ( 'NONE',  ( 2.000000000000000444, 3.464101615137754830, -3.142992957459231018 ) ) ;
#5863=CARTESIAN_POINT ( 'NONE',  ( 2.742827927723449299, 3.035229711104609596, -3.433252694550591233 ) ) ;
#5866=DIRECTION ( 'NONE',  ( 0.000000000000000000, 0.000000000000000000, -1.000000000000000000 ) ) ;
#5879=ADVANCED_FACE ( 'NONE', ( #10897 ), #5780, .F. ) ;
#5887=EDGE_CURVE ( 'NONE', #3798, #12343, #10252, .T. ) ;
#5888=CARTESIAN_POINT ( 'NONE',  ( -2.000000000000007550, -3.464101615137749945, 0.000000000000000000 ) ) ;
#5896=DIRECTION ( 'NONE',  ( 1.000000000000000000, 0.000000000000000000, 0.000000000000000000 ) ) ;
#5914=LINE ( 'NONE', #12652, #7582 ) ;
#5917=CIRCLE ( 'NONE', #9402, 5.384454397937118664 ) ;
#5938=CARTESIAN_POINT ( 'NONE',  ( 2.000000000000008882, 3.464101615137749945, 0.000000000000000000 ) ) ;
#5949=ORIENTED_EDGE ( 'NONE', *, *, #2670, .T. ) ;
#5972=VECTOR ( 'NONE', #13919, 1000.000000000000000 ) ;
#5976=EDGE_LOOP ( 'NONE', ( #7846, #10298, #7473, #3221 ) ) ;
#5978=CARTESIAN_POINT ( 'NONE',  ( 0.000000000000000000, 0.000000000000000000, -4.484454397937119197 ) ) ;
#5989=DIRECTION ( 'NONE',  ( 0.000000000000000000, 0.000000000000000000, -1.000000000000000000 ) ) ;
#5994=CARTESIAN_POINT ( 'NONE',  ( 4.000000000000000000, 2.309401076758497151, -5.000000000000000000 ) ) ;
#6011=CARTESIAN_POINT ( 'NONE',  ( 2.682243648011666703, 3.070208061305304881, -0.04852650426601266831 ) ) ;
#6018=CARTESIAN_POINT ( 'NONE',  ( 1.411581201560190495E-15, 4.862606272033091592, -3.745885042887436622 ) ) ;
#6029=CARTESIAN_POINT ( 'NONE',  ( -6.473970235329672780E-16, -4.862606272033106691, -3.745885042887442395 ) ) ;
#6080=DIRECTION ( 'NONE',  ( 0.000000000000000000, 0.000000000000000000, 1.000000000000000000 ) ) ;
#6081=CARTESIAN_POINT ( 'NONE',  ( 2.500000000000000444, 0.000000000000000000, -5.000000000000000888 ) ) ;
#6086=CARTESIAN_POINT ( 'NONE',  ( -2.807080416178626692, 3.225969019225154444, -3.502507215260441065 ) ) ;
#6095=CIRCLE ( 'NONE', #11894, 0.5155456020628804703 ) ;
#6098=CARTESIAN_POINT ( 'NONE',  ( -4.204015924366189871, 1.626724848190922446, -3.610627190413390419 ) ) ;
#6102=ORIENTED_EDGE ( 'NONE', *, *, #13724, .T. ) ;
#6107=CARTESIAN_POINT ( 'NONE',  ( 0.000000000000000000, 0.000000000000000000, 0.000000000000000000 ) ) ;
#6116=EDGE_LOOP ( 'NONE', ( #11970, #5317, #11756 ) ) ;
#6121=CARTESIAN_POINT ( 'NONE',  ( 1.391697335622810172, 4.043246145443375461, -3.503898532754365913 ) ) ;
#6134=ORIENTED_EDGE ( 'NONE', *, *, #3325, .T. ) ;
#6154=CARTESIAN_POINT ( 'NONE',  ( -4.000000000000000000, 2.309401076758498483, -0.4999999999999927280 ) ) ;
#6156=CARTESIAN_POINT ( 'NONE',  ( -0.5469614295416921346, 4.303013824936271270, -3.535263753543735454 ) ) ;
#6159=PLANE ( 'NONE',  #4061 ) ;
#6163=DIRECTION ( 'NONE',  ( -0.9396926207859138680, 0.000000000000000000, -0.3420201433256536139 ) ) ;
#6229=CARTESIAN_POINT ( 'NONE',  ( 0.02448733951239481094, 4.877042772274728044, -3.751161874094022242 ) ) ;
#6284=FACE_OUTER_BOUND ( 'NONE', #11747, .T. ) ;
#6295=B_SPLINE_CURVE_WITH_KNOTS ( 'NONE', 3,
 ( #12202, #9889, #13290, #126, #60 ),
 .UNSPECIFIED., .F., .F.,
 ( 4, 1, 4 ),
 ( 0.000000000000000000, 0.002309401076758505790, 0.004618802153517011580 ),
 .UNSPECIFIED. ) ;
#6300=B_SPLINE_CURVE_WITH_KNOTS ( 'NONE', 3,
 ( #10178, #4601, #3777, #12615, #9017, #2683 ),
 .UNSPECIFIED., .F., .F.,
 ( 4, 2, 4 ),
 ( 4.336808689942017736E-19, 0.0002095117440864781224, 0.0004190234881729558111 ),
 .UNSPECIFIED. ) ;
#6310=CARTESIAN_POINT ( 'NONE',  ( -4.000000000000000000, -2.309401076758512694, -5.000000000000000000 ) ) ;
#6327=CARTESIAN_POINT ( 'NONE',  ( -4.000000000000000000, 1.700094919196744270, -3.320312364301766017 ) ) ;
#6366=PRODUCT_DEFINITION_CONTEXT ( 'detailed design', #3418, 'design' ) ;
#6371=CARTESIAN_POINT ( 'NONE',  ( 4.197478902586992966, -0.8524102783748346290, -3.505063281295504041 ) ) ;
#6381=ORIENTED_EDGE ( 'NONE', *, *, #10368, .F. ) ;
#6394=CARTESIAN_POINT ( 'NONE',  ( -4.211399284164270895, 2.459729995988205964, -3.751162237960538715 ) ) ;
#6417=CIRCLE ( 'NONE', #11051, 4.000000000000000000 ) ;
#6436=AXIS2_PLACEMENT_3D ( 'NONE', #1671, #5181, #5106 ) ;
#6437=ORIENTED_EDGE ( 'NONE', *, *, #12821, .T. ) ;
#6446=CARTESIAN_POINT ( 'NONE',  ( 0.000000000000000000, 0.000000000000000000, 0.000000000000000000 ) ) ;
#6461=EDGE_LOOP ( 'NONE', ( #8898, #7628, #7057, #8931 ) ) ;
#6465=FACE_OUTER_BOUND ( 'NONE', #10281, .T. ) ;
#6508=ORIENTED_EDGE ( 'NONE', *, *, #11183, .F. ) ;
#6513=CARTESIAN_POINT ( 'NONE',  ( -4.211140560182196957, 2.431303136016537803, -3.745885042887433514 ) ) ;
#6539=DIRECTION ( 'NONE',  ( -1.000000000000000000, 0.000000000000000000, 0.000000000000000000 ) ) ;
#6581=EDGE_CURVE ( 'NONE', #3798, #4511, #5276, .T. ) ;
#6595=CARTESIAN_POINT ( 'NONE',  ( 0.000000000000000000, 0.000000000000000000, 0.000000000000000000 ) ) ;
#6607=CARTESIAN_POINT ( 'NONE',  ( -4.197477534772231955, 0.8522413273724368521, -3.505042416683225692 ) ) ;
#6634=VECTOR ( 'NONE', #4285, 1000.000000000000000 ) ;
#6723=VERTEX_POINT ( 'NONE', #8798 ) ;
#6724=DIRECTION ( 'NONE',  ( 0.5000000000000013323, -0.8660254037844379305, 0.000000000000000000 ) ) ;
#6725=B_SPLINE_CURVE_WITH_KNOTS ( 'NONE', 3,
 ( #10573, #11733, #3821, #1560, #12532, #1635, #2596, #12820 ),
 .UNSPECIFIED., .F., .F.,
 ( 4, 2, 2, 4 ),
 ( 2.465131517390770070E-07, 0.001183067374689869946, 0.001774477805458935659, 0.002365888236228001588 ),
 .UNSPECIFIED. ) ;
#6726=CARTESIAN_POINT ( 'NONE',  ( 2.499999999999999556, 0.000000000000000000, 3.469446951953614189E-15 ) ) ;
#6732=CARTESIAN_POINT ( 'NONE',  ( 1.567478505476134606E-15, 4.618802153517012066, -3.433295621305382905 ) ) ;
#6739=ORIENTED_EDGE ( 'NONE', *, *, #6581, .F. ) ;
#6741=CARTESIAN_POINT ( 'NONE',  ( -3.453038570459499024, -2.625189405340453419, -3.535263753545272891 ) ) ;
#6773=AXIS2_PLACEMENT_3D ( 'NONE', #9355, #3909, #2608 ) ;
#6779=CARTESIAN_POINT ( 'NONE',  ( -2.682243648011671588, -3.070208061305317759, -0.04852650426602272971 ) ) ;
#6787=CARTESIAN_POINT ( 'NONE',  ( 4.203935335434060505, 1.640780671294165272, -3.598452447879202598 ) ) ;
#6806=CARTESIAN_POINT ( 'NONE',  ( -4.000000000000000000, -1.560351142792950618, -0.2242961665059814425 ) ) ;
#6810=CARTESIAN_POINT ( 'NONE',  ( 0.1756481739660539498, -4.720212674038995360, -3.469390959564070620 ) ) ;
#6813=CARTESIAN_POINT ( 'NONE',  ( -3.333333333333332149, -2.694301256218264218, -3.300726591567082036 ) ) ;
#6815=CARTESIAN_POINT ( 'NONE',  ( 4.204015924366189871, -1.626724848190933548, -3.610627190413393084 ) ) ;
#6817=ORIENTED_EDGE ( 'NONE', *, *, #6938, .F. ) ;
#6826=CARTESIAN_POINT ( 'NONE',  ( 0.000000000000000000, 0.000000000000000000, 3.469446951953614189E-15 ) ) ;
#6829=CARTESIAN_POINT ( 'NONE',  ( -6.259644161404859044E-16, -4.618802153517026277, -3.504271511727133248 ) ) ;
#6839=CARTESIAN_POINT ( 'NONE',  ( -3.974357786152442180E-13, 4.796734841935204052, -3.721909803043259579 ) ) ;
#6850=CARTESIAN_POINT ( 'NONE',  ( 3.999999999999998224, 2.472263674411418588, -3.687027874309861897 ) ) ;
#6876=CARTESIAN_POINT ( 'NONE',  ( 4.235886605889389145, 2.417314728048528760, -3.751161874094018245 ) ) ;
#6922=PRODUCT ( 'hex flange nut gradea_iso_ISO - 4161 - M5 - N', 'hex flange nut gradea_iso_ISO - 4161 - M5 - N', '', ( #6977 ) ) ;
#6926=CARTESIAN_POINT ( 'NONE',  ( 1.317756351988342622, -3.857995168970215438, -0.04852650426602527628 ) ) ;
#6928=EDGE_CURVE ( 'NONE', #32, #10282, #1274, .T. ) ;
#6930=CARTESIAN_POINT ( 'NONE',  ( 1.411581201560190495E-15, 4.862606272033091592, -3.745885042887436622 ) ) ;
#6938=EDGE_CURVE ( 'NONE', #10282, #32, #5917, .T. ) ;
#6939=EDGE_CURVE ( 'NONE', #8960, #3920, #3166, .T. ) ;
#6948=CARTESIAN_POINT ( 'NONE',  ( 0.5636800770130377947, 4.293361309317166530, -3.531542292954102713 ) ) ;
#6950=CARTESIAN_POINT ( 'NONE',  ( 0.000000000000000000, 0.000000000000000000, -4.974599999999998801 ) ) ;
#6977=PRODUCT_CONTEXT ( 'NONE', #10074, 'mechanical' ) ;
#6984=VERTEX_POINT ( 'NONE', #7766 ) ;
#6991=CARTESIAN_POINT ( 'NONE',  ( -6.259644161404860030E-16, -4.618802153517027165, -5.000000000000000000 ) ) ;
#7009=STYLED_ITEM ( 'NONE', ( #2556 ), #12151 ) ;
#7012=DIRECTION ( 'NONE',  ( -0.8660254037844373753, 0.5000000000000021094, 0.000000000000000000 ) ) ;
#7028=FACE_OUTER_BOUND ( 'NONE', #8917, .T. ) ;
#7036=ORIENTED_EDGE ( 'NONE', *, *, #13724, .F. ) ;
#7045=CYLINDRICAL_SURFACE ( 'NONE', #12952, 2.500000000000000444 ) ;
#7053=ADVANCED_FACE ( 'NONE', ( #2839 ), #13797, .T. ) ;
#7057=ORIENTED_EDGE ( 'NONE', *, *, #10321, .F. ) ;
#7094=FACE_OUTER_BOUND ( 'NONE', #13429, .T. ) ;
#7121=CARTESIAN_POINT ( 'NONE',  ( -1.999999999999999556, 3.464101615137754830, -3.142992957459232795 ) ) ;
#7145=FACE_OUTER_BOUND ( 'NONE', #11095, .T. ) ;
#7155=ORIENTED_EDGE ( 'NONE', *, *, #11156, .F. ) ;
#7160=LINE ( 'NONE', #4781, #5513 ) ;
#7174=( BOUNDED_SURFACE ( )  B_SPLINE_SURFACE ( 3, 2, ( 
 ( #985, #5434, #9858 ),
 ( #12319, #13529, #7948 ),
 ( #3476, #4497, #10211 ),
 ( #10142, #11308, #7877 ),
 ( #9121, #13464, #4712 ),
 ( #38, #243, #4634 ) ),
 .UNSPECIFIED., .F., .F., .T. ) 
 B_SPLINE_SURFACE_WITH_KNOTS ( ( 4, 2, 4 ),
 ( 3, 3 ),
 ( 0.02032853247518126918, 0.02278863295364821906, 0.02524873343211517240 ),
 ( 0.000000000000000000, 1.000000000000000000 ),
 .UNSPECIFIED. ) 
 GEOMETRIC_REPRESENTATION_ITEM ( )  RATIONAL_B_SPLINE_SURFACE ( (
 ( 1.000000000000000000, 0.8047781615896837382, 1.000000000000000000),
 ( 1.000000000000000000, 0.8123767586289252218, 1.000000000000000000),
 ( 1.000000000000000000, 0.8190662415564388121, 1.000000000000000000),
 ( 1.000000000000000000, 0.8192361015669026303, 1.000000000000000000),
 ( 1.000000000000000000, 0.8126135807103900266, 1.000000000000000000),
 ( 1.000000000000000000, 0.8047712338318593339, 1.000000000000000000) ) ) 
 REPRESENTATION_ITEM ( '' )  SURFACE ( )  );
#7201=B_SPLINE_CURVE_WITH_KNOTS ( 'NONE', 3,
 ( #6154, #4860, #13762, #13691, #2673, #1261, #1335, #3598 ),
 .UNSPECIFIED., .F., .F.,
 ( 4, 2, 2, 4 ),
 ( 2.465131517071352357E-07, 0.001183067374689843057, 0.001774477805458910071, 0.002365888236227977302 ),
 .UNSPECIFIED. ) ;
#7245=CARTESIAN_POINT ( 'NONE',  ( 4.000000000000000000, 2.309401076758515803, -0.4999999999999995559 ) ) ;
#7247=PRODUCT_DEFINITION_FORMATION_WITH_SPECIFIED_SOURCE ( 'ANY', '', #6922, .NOT_KNOWN. ) ;
#7249=FACE_OUTER_BOUND ( 'NONE', #5374, .T. ) ;
#7254=CARTESIAN_POINT ( 'NONE',  ( -4.211140560182196957, 2.431303136016537803, -3.745885042887433514 ) ) ;
#7264=EDGE_LOOP ( 'NONE', ( #3502, #8704, #12575 ) ) ;
#7269=CARTESIAN_POINT ( 'NONE',  ( 2.687328764639642653, -3.067272167851299969, -0.05923475698271395140 ) ) ;
#7310=CARTESIAN_POINT ( 'NONE',  ( -1.360585162435467455, 4.061296242128285883, -3.505054077164959203 ) ) ;
#7319=EDGE_LOOP ( 'NONE', ( #7418, #11344, #12553, #11537 ) ) ;
#7340=ORIENTED_EDGE ( 'NONE', *, *, #8607, .F. ) ;
#7348=CIRCLE ( 'NONE', #8743, 4.000000000000000000 ) ;
#7361=CARTESIAN_POINT ( 'NONE',  ( -5.384454397937118664, 6.702023979852544604E-16, -5.000000000000000000 ) ) ;
#7388=CIRCLE ( 'NONE', #7847, 4.000000000000000000 ) ;
#7394=CARTESIAN_POINT ( 'NONE',  ( 1.567478505476134606E-15, 4.618802153517012066, -3.433295621305382905 ) ) ;
#7418=ORIENTED_EDGE ( 'NONE', *, *, #2300, .F. ) ;
#7430=AXIS2_PLACEMENT_3D ( 'NONE', #10222, #11449, #1567 ) ;
#7449=EDGE_LOOP ( 'NONE', ( #2118, #4813, #7501, #3612, #7036 ) ) ;
#7473=ORIENTED_EDGE ( 'NONE', *, *, #4191, .T. ) ;
#7488=ORIENTED_EDGE ( 'NONE', *, *, #4171, .T. ) ;
#7501=ORIENTED_EDGE ( 'NONE', *, *, #2723, .F. ) ;
#7525=ORIENTED_EDGE ( 'NONE', *, *, #11156, .T. ) ;
#7535=CARTESIAN_POINT ( 'NONE',  ( 2.100000000000000089, 0.000000000000000000, -5.000000000000000000 ) ) ;
#7536=EDGE_LOOP ( 'NONE', ( #13213, #14184, #3534, #8588, #12075 ) ) ;
#7537=DIRECTION ( 'NONE',  ( -0.000000000000000000, -0.000000000000000000, 1.000000000000000000 ) ) ;
#7542=CARTESIAN_POINT ( 'NONE',  ( -4.000000000000000000, -0.8232339106130515116, -3.430630286862743183 ) ) ;
#7561=CARTESIAN_POINT ( 'NONE',  ( 0.000000000000000000, 0.000000000000000000, 0.000000000000000000 ) ) ;
#7569=AXIS2_PLACEMENT_3D ( 'NONE', #6991, #6724, #11153 ) ;
#7574=CARTESIAN_POINT ( 'NONE',  ( 0.000000000000000000, 0.000000000000000000, -4.000000000000000000 ) ) ;
#7582=VECTOR ( 'NONE', #2652, 1000.000000000000114 ) ;
#7588=CONICAL_SURFACE ( 'NONE', #3647, 5.560781378645573980, 1.221730476396046816 ) ;
#7614=CARTESIAN_POINT ( 'NONE',  ( 8.673617379884035472E-16, 4.618802153517012954, 0.000000000000000000 ) ) ;
#7628=ORIENTED_EDGE ( 'NONE', *, *, #10987, .T. ) ;
#7644=CARTESIAN_POINT ( 'NONE',  ( -3.349226789952655547, -2.685125164760744809, -0.2236248678334863682 ) ) ;
#7660=CARTESIAN_POINT ( 'NONE',  ( 0.000000000000000000, 0.000000000000000000, -0.2800830152838844622 ) ) ;
#7695=AXIS2_PLACEMENT_3D ( 'NONE', #13809, #11500, #8301 ) ;
#7699=EDGE_CURVE ( 'NONE', #4974, #8960, #3975, .T. ) ;
#7708=DIRECTION ( 'NONE',  ( 0.000000000000000000, 0.000000000000000000, -1.000000000000000000 ) ) ;
#7712=ADVANCED_FACE ( 'NONE', ( #10218 ), #14208, .F. ) ;
#7734=ORIENTED_EDGE ( 'NONE', *, *, #7699, .T. ) ;
#7755=CARTESIAN_POINT ( 'NONE',  ( -6.259644161404860030E-16, -4.618802153517027165, -3.433295621305388234 ) ) ;
#7766=CARTESIAN_POINT ( 'NONE',  ( 4.000000000000000000, 2.309401076758497151, -3.433295621305379353 ) ) ;
#7770=CARTESIAN_POINT ( 'NONE',  ( -6.473970235329672780E-16, -4.862606272033106691, -3.745885042887442395 ) ) ;
#7773=CARTESIAN_POINT ( 'NONE',  ( 0.000000000000000000, 0.000000000000000000, -4.000000000000000000 ) ) ;
#7795=DIRECTION ( 'NONE',  ( 0.000000000000000000, 0.000000000000000000, -1.000000000000000000 ) ) ;
#7798=PLANE ( 'NONE',  #7569 ) ;
#7816=EDGE_CURVE ( 'NONE', #12343, #4511, #2071, .T. ) ;
#7820=EDGE_CURVE ( 'NONE', #13737, #5507, #992, .T. ) ;
#7822=AXIS2_PLACEMENT_3D ( 'NONE', #12293, #6, #4471 ) ;
#7846=ORIENTED_EDGE ( 'NONE', *, *, #10987, .F. ) ;
#7847=AXIS2_PLACEMENT_3D ( 'NONE', #6446, #1940, #4201 ) ;
#7849=ADVANCED_FACE ( 'NONE', ( #974 ), #7798, .T. ) ;
#7852=DIRECTION ( 'NONE',  ( 0.000000000000000000, 0.000000000000000000, 1.000000000000000000 ) ) ;
#7865=DIRECTION ( 'NONE',  ( 0.000000000000000000, 0.000000000000000000, 1.000000000000000000 ) ) ;
#7869=DIRECTION ( 'NONE',  ( -1.000000000000000000, 0.000000000000000000, 0.000000000000000000 ) ) ;
#7877=CARTESIAN_POINT ( 'NONE',  ( 2.807080416178989513, -3.225969019225150003, -3.502507215260505014 ) ) ;
#7903=CARTESIAN_POINT ( 'NONE',  ( 0.000000000000000000, 0.000000000000000000, -5.000000000000000000 ) ) ;
#7911=DIRECTION ( 'NONE',  ( -0.000000000000000000, -0.000000000000000000, 1.000000000000000000 ) ) ;
#7937=LINE ( 'NONE', #13383, #14073 ) ;
#7948=CARTESIAN_POINT ( 'NONE',  ( 0.6640947660595348800, -4.471078309994175548, -3.602146406945708090 ) ) ;
#7973=EDGE_CURVE ( 'NONE', #924, #2940, #3793, .T. ) ;
#7985=CARTESIAN_POINT ( 'NONE',  ( 0.000000000000000000, 0.000000000000000000, -4.694516984716113228 ) ) ;
#7988=AXIS2_PLACEMENT_3D ( 'NONE', #7903, #1084, #1301 ) ;
#7994=CARTESIAN_POINT ( 'NONE',  ( 4.000000000001088907, 1.658577278524410170, -3.531553309554541720 ) ) ;
#7997=EDGE_CURVE ( 'NONE', #8807, #3312, #5268, .T. ) ;
#8025=CARTESIAN_POINT ( 'NONE',  ( 0.5449313310647804220, 4.304185902836899835, -3.316620875263383894 ) ) ;
#8034=CARTESIAN_POINT ( 'NONE',  ( 4.197393957002303999, 7.772902908466098641E-14, -3.503767560748929810 ) ) ;
#8082=CARTESIAN_POINT ( 'NONE',  ( -2.688821387764050996E-14, -4.618802153517012954, -0.4999999999999995559 ) ) ;
#8101=CARTESIAN_POINT ( 'NONE',  ( 0.1410422978106145031, -4.700232962125109104, -3.687027686973628704 ) ) ;
#8145=CARTESIAN_POINT ( 'NONE',  ( -4.000000000000000000, 2.309401076758498483, -5.000000000000000000 ) ) ;
#8181=ORIENTED_EDGE ( 'NONE', *, *, #5187, .T. ) ;
#8195=DIRECTION ( 'NONE',  ( 1.000000000000000000, 0.000000000000000000, 0.000000000000000000 ) ) ;
#8232=ORIENTED_EDGE ( 'NONE', *, *, #11033, .F. ) ;
#8233=CARTESIAN_POINT ( 'NONE',  ( -4.000000000000000000, -2.309401076758512694, -3.433295621305382461 ) ) ;
#8274=AXIS2_PLACEMENT_3D ( 'NONE', #484, #3570, #12623 ) ;
#8295=ORIENTED_EDGE ( 'NONE', *, *, #12980, .F. ) ;
#8298=CARTESIAN_POINT ( 'NONE',  ( -3.999999999999999112, 1.539600717838996324, -3.300726591567078039 ) ) ;
#8301=DIRECTION ( 'NONE',  ( 1.000000000000000000, 0.000000000000000000, 0.000000000000000000 ) ) ;
#8349=CIRCLE ( 'NONE', #13463, 2.499999999999999556 ) ;
#8363=DIRECTION ( 'NONE',  ( -1.000000000000000000, 0.000000000000000000, 0.000000000000000000 ) ) ;
#8364=DIRECTION ( 'NONE',  ( -1.000000000000000000, 0.000000000000000000, 0.000000000000000000 ) ) ;
#8395=PLANE ( 'NONE',  #6773 ) ;
#8399=CARTESIAN_POINT ( 'NONE',  ( -4.175648173966055587, 2.207990556236529844, -3.469390959564062626 ) ) ;
#8402=ORIENTED_EDGE ( 'NONE', *, *, #11033, .T. ) ;
#8457=CYLINDRICAL_SURFACE ( 'NONE', #431, 2.100000000000000089 ) ;
#8464=CARTESIAN_POINT ( 'NONE',  ( -6.473970235329672780E-16, -4.862606272033106691, -3.745885042887442395 ) ) ;
#8469=ADVANCED_FACE ( 'NONE', ( #5236 ), #5060, .T. ) ;
#8475=DIRECTION ( 'NONE',  ( -1.000000000000000000, 1.224646799147352714E-16, 0.000000000000000000 ) ) ;
#8510=CARTESIAN_POINT ( 'NONE',  ( 2.804994570502171047, 3.229033611042449792, -3.526374918436834704 ) ) ;
#8519=B_SPLINE_CURVE_WITH_KNOTS ( 'NONE', 3,
 ( #5004, #4055, #2977, #2898, #13838, #3912, #2827, #7245 ),
 .UNSPECIFIED., .F., .F.,
 ( 4, 2, 2, 4 ),
 ( 0.005725059856848645212, 0.006314084072593634418, 0.006903108288338624492, 0.008081156719828603771 ),
 .UNSPECIFIED. ) ;
#8545=CARTESIAN_POINT ( 'NONE',  ( 4.204115023516791005, -1.660442669500199919, -3.602151381774560068 ) ) ;
#8588=ORIENTED_EDGE ( 'NONE', *, *, #1391, .T. ) ;
#8607=EDGE_CURVE ( 'NONE', #11069, #2351, #1079, .T. ) ;
#8652=CARTESIAN_POINT ( 'NONE',  ( -4.000000000000000000, 2.309401076758498483, -3.433295621305379353 ) ) ;
#8656=EDGE_LOOP ( 'NONE', ( #11795, #1974, #2348, #5287, #594 ) ) ;
#8668=DIRECTION ( 'NONE',  ( 0.000000000000000000, 0.000000000000000000, -1.000000000000000000 ) ) ;
#8673=B_SPLINE_CURVE_WITH_KNOTS ( 'NONE', 3,
 ( #10933, #3389, #9986, #890, #4186, #4480 ),
 .UNSPECIFIED., .F., .F.,
 ( 4, 2, 4 ),
 ( -3.640115492409406142E-06, 0.0002066546034003385283, 0.0004169493222930864334 ),
 .UNSPECIFIED. ) ;
#8685=EDGE_CURVE ( 'NONE', #5289, #13737, #7160, .T. ) ;
#8692=ORIENTED_EDGE ( 'NONE', *, *, #7820, .T. ) ;
#8704=ORIENTED_EDGE ( 'NONE', *, *, #3623, .T. ) ;
#8710=CARTESIAN_POINT ( 'NONE',  ( -4.000000000000000000, -2.472261339043343220, -3.687027428081192326 ) ) ;
#8739=ORIENTED_EDGE ( 'NONE', *, *, #9631, .F. ) ;
#8741=CARTESIAN_POINT ( 'NONE',  ( 1.393927851585479161, -4.043713361053543842, -3.526374918436840922 ) ) ;
#8743=AXIS2_PLACEMENT_3D ( 'NONE', #6107, #9593, #12702 ) ;
#8744=VERTEX_POINT ( 'NONE', #1566 ) ;
#8769=MANIFOLD_SOLID_BREP ( 'EndChamfer', #13764 ) ;
#8785=CARTESIAN_POINT ( 'NONE',  ( -4.000000000000000000, -1.680117682357936904, -3.316611593218794951 ) ) ;
#8791=VERTEX_POINT ( 'NONE', #4198 ) ;
#8798=CARTESIAN_POINT ( 'NONE',  ( -4.197393957002303999, -7.773935952363655451E-14, -3.503767560748929810 ) ) ;
#8805=AXIS2_PLACEMENT_3D ( 'NONE', #1469, #9248, #9321 ) ;
#8807=VERTEX_POINT ( 'NONE', #2009 ) ;
#8818=EDGE_CURVE ( 'NONE', #4036, #5289, #10715, .T. ) ;
#8832=CARTESIAN_POINT ( 'NONE',  ( 1.828356344711641102, 3.563200125723180900, -5.433716356636336675E-16 ) ) ;
#8878=LINE ( 'NONE', #3511, #5143 ) ;
#8898=ORIENTED_EDGE ( 'NONE', *, *, #6928, .T. ) ;
#8906=CARTESIAN_POINT ( 'NONE',  ( 0.6448876103708359731, 4.246476118072354922, -0.2256878752776725616 ) ) ;
#8908=CARTESIAN_POINT ( 'NONE',  ( 0.000000000000000000, 0.000000000000000000, 0.000000000000000000 ) ) ;
#8917=EDGE_LOOP ( 'NONE', ( #11847, #9782, #13738, #3105 ) ) ;
#8931=ORIENTED_EDGE ( 'NONE', *, *, #4191, .F. ) ;
#8939=CARTESIAN_POINT ( 'NONE',  ( 4.154306624730864428, 2.398490048084778170, -3.721999068284300272 ) ) ;
#8942=EDGE_CURVE ( 'NONE', #5507, #2488, #6417, .T. ) ;
#8949=EDGE_LOOP ( 'NONE', ( #4017, #5217, #14204, #5277 ) ) ;
#8960=VERTEX_POINT ( 'NONE', #6726 ) ;
#8983=EDGE_LOOP ( 'NONE', ( #3654, #4517, #11850, #12910 ) ) ;
#9014=AXIS2_PLACEMENT_3D ( 'NONE', #5994, #10420, #7012 ) ;
#9017=CARTESIAN_POINT ( 'NONE',  ( 4.154306624730763176, -2.398490048084970461, -3.721999068284303824 ) ) ;
#9063=CARTESIAN_POINT ( 'NONE',  ( 3.679171394226031122, 2.494631558665830973, -0.3503314178412474389 ) ) ;
#9121=CARTESIAN_POINT ( 'NONE',  ( 3.455068668934414777, -2.624017327439094327, -3.316620875263732504 ) ) ;
#9127=CARTESIAN_POINT ( 'NONE',  ( -1.390230914382372118, -4.043987460488664532, -3.502507215260523665 ) ) ;
#9130=CARTESIAN_POINT ( 'NONE',  ( 0.000000000000000000, 0.000000000000000000, -4.974599999999998801 ) ) ;
#9132=CARTESIAN_POINT ( 'NONE',  ( 4.000000000000000000, 2.309401076758515803, -0.4999999999999995559 ) ) ;
#9139=EDGE_CURVE ( 'NONE', #4036, #12837, #449, .T. ) ;
#9155=CONICAL_SURFACE ( 'NONE', #9854, 4.000000000000000000, 0.8911886515913786111 ) ;
#9161=DIRECTION ( 'NONE',  ( -1.000000000000000000, 0.000000000000000000, 0.000000000000000000 ) ) ;
#9165=CARTESIAN_POINT ( 'NONE',  ( 1.734723475976807094E-15, 4.618802153517012954, -0.4999999999999995559 ) ) ;
#9182=VECTOR ( 'NONE', #7852, 1000.000000000000000 ) ;
#9194=VECTOR ( 'NONE', #4022, 1000.000000000000000 ) ;
#9198=CARTESIAN_POINT ( 'NONE',  ( -0.02511973781850462134, 4.877415612947412882, -3.751298745799839462 ) ) ;
#9208=AXIS2_PLACEMENT_3D ( 'NONE', #9256, #12812, #2879 ) ;
#9213=EDGE_LOOP ( 'NONE', ( #460, #9857, #7734, #5244 ) ) ;
#9215=MECHANICAL_DESIGN_GEOMETRIC_PRESENTATION_REPRESENTATION('',(#2232),#9697);
#9224=CARTESIAN_POINT ( 'NONE',  ( -6.259644161404860030E-16, -4.618802153517027165, -3.433295621305388234 ) ) ;
#9225=( LENGTH_UNIT ( ) NAMED_UNIT ( * ) SI_UNIT ( .MILLI., .METRE. ) );
#9231=ORIENTED_EDGE ( 'NONE', *, *, #14027, .T. ) ;
#9237=CARTESIAN_POINT ( 'NONE',  ( 2.500000000000000444, 0.000000000000000000, -25.03750572909317285 ) ) ;
#9244=CARTESIAN_POINT ( 'NONE',  ( 0.000000000000000000, 0.000000000000000000, 0.000000000000000000 ) ) ;
#9248=DIRECTION ( 'NONE',  ( -0.5000000000000016653, 0.8660254037844378194, 0.000000000000000000 ) ) ;
#9256=CARTESIAN_POINT ( 'NONE',  ( 0.000000000000000000, 0.000000000000000000, 0.000000000000000000 ) ) ;
#9278=FACE_OUTER_BOUND ( 'NONE', #4300, .T. ) ;
#9295=CIRCLE ( 'NONE', #10928, 4.000000000000000000 ) ;
#9296=CARTESIAN_POINT ( 'NONE',  ( 0.000000000000000000, 0.000000000000000000, 0.000000000000000000 ) ) ;
#9307=SHAPE_REPRESENTATION ( 'hex flange nut gradea_iso_ISO - 4161 - M5 - N', ( #14039 ), #1206 ) ;
#9321=DIRECTION ( 'NONE',  ( -0.8660254037844377084, -0.5000000000000015543, 0.000000000000000000 ) ) ;
#9322=VECTOR ( 'NONE', #13907, 999.9999999999998863 ) ;
#9352=CARTESIAN_POINT ( 'NONE',  ( -0.5636800770129166693, -4.293361309317430319, -3.531542292955206275 ) ) ;
#9355=CARTESIAN_POINT ( 'NONE',  ( -4.000000000000000000, -2.309401076758512694, -5.000000000000000000 ) ) ;
#9365=CARTESIAN_POINT ( 'NONE',  ( -1.747541505913277282, 3.837784562140256650, -3.503702292528906526 ) ) ;
#9402=AXIS2_PLACEMENT_3D ( 'NONE', #12344, #2406, #11192 ) ;
#9418=DIRECTION ( 'NONE',  ( 0.000000000000000000, 0.000000000000000000, 1.000000000000000000 ) ) ;
#9425=CARTESIAN_POINT ( 'NONE',  ( -4.236525694536558362, 2.416953475386465211, -3.751298745799836354 ) ) ;
#9432=ORIENTED_EDGE ( 'NONE', *, *, #9760, .F. ) ;
#9447=CONICAL_SURFACE ( 'NONE', #8274, 2.500000000000000888, 0.9599310885968785900 ) ;
#9457=ORIENTED_EDGE ( 'NONE', *, *, #12224, .T. ) ;
#9465=TOROIDAL_SURFACE ( 'NONE', #2043, 5.384454397937118664, 0.5155456020628804703 ) ;
#9479=FACE_OUTER_BOUND ( 'NONE', #1443, .T. ) ;
#9503=DIRECTION ( 'NONE',  ( -1.000000000000000000, 0.000000000000000000, 0.000000000000000000 ) ) ;
#9535=LINE ( 'NONE', #13946, #9194 ) ;
#9545=CARTESIAN_POINT ( 'NONE',  ( -4.000000000000000000, -7.806255641895631925E-15, -3.142992957459232350 ) ) ;
#9551=DIRECTION ( 'NONE',  ( 0.000000000000000000, 0.000000000000000000, 1.000000000000000000 ) ) ;
#9565=MECHANICAL_DESIGN_GEOMETRIC_PRESENTATION_REPRESENTATION('',(#7009),#1641);
#9571=CARTESIAN_POINT ( 'NONE',  ( -3.510273485745307287, -2.827716139362669967, -3.610536846335890004 ) ) ;
#9575=CARTESIAN_POINT ( 'NONE',  ( -1.243802165048909503, 3.900692638707381921, -3.223146290109805800 ) ) ;
#9582=CARTESIAN_POINT ( 'NONE',  ( -5.560781378645573980, 0.000000000000000000, -4.000000000000000000 ) ) ;
#9593=DIRECTION ( 'NONE',  ( -0.000000000000000000, -0.000000000000000000, 1.000000000000000000 ) ) ;
#9598=ADVANCED_FACE ( 'NONE', ( #4830 ), #10942, .T. ) ;
#9604=ORIENTED_EDGE ( 'NONE', *, *, #4391, .F. ) ;
#9611=DIRECTION ( 'NONE',  ( -1.000000000000000000, 0.000000000000000000, 0.000000000000000000 ) ) ;
#9626=B_SPLINE_CURVE_WITH_KNOTS ( 'NONE', 3,
 ( #9906, #8298, #9545, #12868, #2874 ),
 .UNSPECIFIED., .F., .F.,
 ( 4, 1, 4 ),
 ( 0.000000000000000000, 0.002309401076758505790, 0.004618802153517011580 ),
 .UNSPECIFIED. ) ;
#9631=EDGE_CURVE ( 'NONE', #13395, #10991, #1067, .T. ) ;
#9639=CARTESIAN_POINT ( 'NONE',  ( 4.000000000000000000, -1.700175430507292473, -3.320327275037661785 ) ) ;
#9651=CARTESIAN_POINT ( 'NONE',  ( -2.688821387764050996E-14, -4.618802153517012954, -0.4999999999999995559 ) ) ;
#9697=( GEOMETRIC_REPRESENTATION_CONTEXT ( 3 ) GLOBAL_UNCERTAINTY_ASSIGNED_CONTEXT ( ( #2864 ) ) GLOBAL_UNIT_ASSIGNED_CONTEXT ( ( #10947, #1867, #10735 ) ) REPRESENTATION_CONTEXT ( 'NONE', 'WORKASPACE' ) );
#9705=EDGE_LOOP ( 'NONE', ( #11622, #646, #714 ) ) ;
#9731=CARTESIAN_POINT ( 'NONE',  ( -4.000000000000000888, 1.563622288139195238, -0.2253451193528307472 ) ) ;
#9738=CARTESIAN_POINT ( 'NONE',  ( -4.197312064133472020, -0.8182229787990021874, -3.502518405183886685 ) ) ;
#9743=CONICAL_SURFACE ( 'NONE', #3707, 2.059999999999998721, 0.9599310885968738161 ) ;
#9760=EDGE_CURVE ( 'NONE', #1149, #12343, #13874, .T. ) ;
#9775=EDGE_CURVE ( 'NONE', #931, #4036, #1307, .T. ) ;
#9782=ORIENTED_EDGE ( 'NONE', *, *, #12092, .T. ) ;
#9810=CARTESIAN_POINT ( 'NONE',  ( 0.000000000000000000, 0.000000000000000000, -4.974599999999998801 ) ) ;
#9835=B_SPLINE_CURVE_WITH_KNOTS ( 'NONE', 3,
 ( #12988, #771, #1657, #6098, #3921, #7254 ),
 .UNSPECIFIED., .F., .F.,
 ( 4, 2, 4 ),
 ( 0.002452478801916376308, 0.003676905084148007850, 0.004901331366379639391 ),
 .UNSPECIFIED. ) ;
#9850=EDGE_CURVE ( 'NONE', #2351, #11069, #10707, .T. ) ;
#9854=AXIS2_PLACEMENT_3D ( 'NONE', #11197, #14231, #14189 ) ;
#9857=ORIENTED_EDGE ( 'NONE', *, *, #11588, .T. ) ;
#9858=CARTESIAN_POINT ( 'NONE',  ( -0.02448733951239248641, -4.877042772274742255, -3.751161874094027571 ) ) ;
#9869=CARTESIAN_POINT ( 'NONE',  ( -4.140404888673278272, -2.228338276487456415, -3.686887068327035166 ) ) ;
#9874=CARTESIAN_POINT ( 'NONE',  ( -4.000000000000000000, -0.8382240730041925492, -3.220610619767135141 ) ) ;
#9889=CARTESIAN_POINT ( 'NONE',  ( 3.999999999999999112, -1.539600717839012978, -3.300726591567080703 ) ) ;
#9906=CARTESIAN_POINT ( 'NONE',  ( -4.000000000000000000, 2.309401076758498483, -3.433295621305379353 ) ) ;
#9913=CARTESIAN_POINT ( 'NONE',  ( 2.100000000000000089, 0.000000000000000000, -0.2800830152838844622 ) ) ;
#9932=ORIENTED_EDGE ( 'NONE', *, *, #5887, .T. ) ;
#9964=CARTESIAN_POINT ( 'NONE',  ( 4.000000000000000000, -2.309401076758516691, -0.4999999999999995559 ) ) ;
#9965=EDGE_CURVE ( 'NONE', #1964, #3920, #10583, .T. ) ;
#9971=ORIENTED_EDGE ( 'NONE', *, *, #12798, .F. ) ;
#9976=ADVANCED_FACE ( 'NONE', ( #9278 ), #8395, .T. ) ;
#9986=CARTESIAN_POINT ( 'NONE',  ( -4.101948962586059899, -2.368261337751176754, -3.681124513963741851 ) ) ;
#9994=CARTESIAN_POINT ( 'NONE',  ( 4.000000000000000000, -2.309401076758516691, -0.4999999999999995559 ) ) ;
#10018=CIRCLE ( 'NONE', #7695, 5.560781378645573980 ) ;
#10036=CARTESIAN_POINT ( 'NONE',  ( 4.211140560182196957, 2.431303136016536470, -3.745885042887433514 ) ) ;
#10038=FACE_OUTER_BOUND ( 'NONE', #9705, .T. ) ;
#10049=EDGE_CURVE ( 'NONE', #11323, #3798, #7201, .T. ) ;
#10074=APPLICATION_CONTEXT ( 'automotive_design' ) ;
#10102=VERTEX_POINT ( 'NONE', #13452 ) ;
#10127=ORIENTED_EDGE ( 'NONE', *, *, #7997, .T. ) ;
#10131=CARTESIAN_POINT ( 'NONE',  ( 2.500000000000000888, 3.061616997868384127E-16, -4.974599999999998801 ) ) ;
#10141=ORIENTED_EDGE ( 'NONE', *, *, #6939, .F. ) ;
#10142=CARTESIAN_POINT ( 'NONE',  ( 2.725741868436127202, -3.045094352033990148, -3.220599429844051453 ) ) ;
#10154=ORIENTED_EDGE ( 'NONE', *, *, #10368, .T. ) ;
#10178=CARTESIAN_POINT ( 'NONE',  ( 4.000000000000000000, -2.309401076758514915, -3.433295621305383349 ) ) ;
#10184=AXIS2_PLACEMENT_3D ( 'NONE', #2646, #11428, #360 ) ;
#10201=LINE ( 'NONE', #10131, #10877 ) ;
#10205=ADVANCED_FACE ( 'NONE', ( #7145 ), #13708, .T. ) ;
#10211=CARTESIAN_POINT ( 'NONE',  ( 1.360585162435110629, -4.061296242128317857, -3.505054077164905024 ) ) ;
#10218=FACE_OUTER_BOUND ( 'NONE', #8949, .T. ) ;
#10222=CARTESIAN_POINT ( 'NONE',  ( 0.000000000000000000, 0.000000000000000000, -5.000000000000000000 ) ) ;
#10225=CARTESIAN_POINT ( 'NONE',  ( 4.211140560182196957, -2.431303136016555122, -3.745885042887436622 ) ) ;
#10232=DIRECTION ( 'NONE',  ( -1.000000000000000000, 0.000000000000000000, 0.000000000000000000 ) ) ;
#10252=B_SPLINE_CURVE_WITH_KNOTS ( 'NONE', 3,
 ( #3284, #5383, #1071, #3360, #13131, #12997 ),
 .UNSPECIFIED., .F., .F.,
 ( 4, 2, 4 ),
 ( 0.002365888236227977302, 0.003551327329835078910, 0.004736766423442180518 ),
 .UNSPECIFIED. ) ;
#10255=DIRECTION ( 'NONE',  ( -0.000000000000000000, -0.000000000000000000, 1.000000000000000000 ) ) ;
#10281=EDGE_LOOP ( 'NONE', ( #9457, #12152, #12402, #4672 ) ) ;
#10282=VERTEX_POINT ( 'NONE', #7361 ) ;
#10285=CARTESIAN_POINT ( 'NONE',  ( -0.1410422978106123659, 4.700232962125094893, -3.687027686973624707 ) ) ;
#10290=CARTESIAN_POINT ( 'NONE',  ( 2.344047193898588954, 3.265465875126468021, -5.031375706690542042E-16 ) ) ;
#10298=ORIENTED_EDGE ( 'NONE', *, *, #6938, .T. ) ;
#10306=CARTESIAN_POINT ( 'NONE',  ( 4.211140560182196957, 2.431303136016536470, -3.745885042887433514 ) ) ;
#10321=EDGE_CURVE ( 'NONE', #10991, #8744, #10018, .T. ) ;
#10339=B_SPLINE_CURVE_WITH_KNOTS ( 'NONE', 3,
 ( #2307, #12171, #5855, #13527, #6732 ),
 .UNSPECIFIED., .F., .F.,
 ( 4, 1, 4 ),
 ( 0.000000000000000000, 0.002309401076758505356, 0.004618802153517010713 ),
 .UNSPECIFIED. ) ;
#10355=CARTESIAN_POINT ( 'NONE',  ( 2.836893136758676270, 3.208949435745843903, -3.505054077164911241 ) ) ;
#10368=EDGE_CURVE ( 'NONE', #8791, #2471, #4953, .T. ) ;
#10385=PLANE ( 'NONE',  #6436 ) ;
#10398=CARTESIAN_POINT ( 'NONE',  ( 4.211140560182196957, 2.431303136016536470, -3.745885042887433514 ) ) ;
#10417=B_SPLINE_CURVE_WITH_KNOTS ( 'NONE', 3,
 ( #8034, #4650, #1361, #6815, #189, #10225 ),
 .UNSPECIFIED., .F., .F.,
 ( 4, 2, 4 ),
 ( 0.002452478801916361129, 0.003676905084148001344, 0.004901331366379641126 ),
 .UNSPECIFIED. ) ;
#10419=B_SPLINE_CURVE_WITH_KNOTS ( 'NONE', 3,
 ( #11553, #1601, #12787, #2857, #7269, #11698, #650, #11849 ),
 .UNSPECIFIED., .F., .F.,
 ( 4, 2, 2, 4 ),
 ( 2.465131517071610173E-07, 0.001183067374689837636, 0.001774477805458902699, 0.002365888236227967761 ),
 .UNSPECIFIED. ) ;
#10420=DIRECTION ( 'NONE',  ( 0.5000000000000022204, 0.8660254037844374864, -0.000000000000000000 ) ) ;
#10429=CARTESIAN_POINT ( 'NONE',  ( -2.100000000000000089, 2.571758278209441957E-16, -4.694516984716113228 ) ) ;
#10432=CARTESIAN_POINT ( 'NONE',  ( 1.274258131564866448, 3.883108878240963513, -3.220599429844046568 ) ) ;
#10444=EDGE_LOOP ( 'NONE', ( #8181, #10127 ) ) ;
#10473=DIRECTION ( 'NONE',  ( 1.000000000000000000, 0.000000000000000000, 0.000000000000000000 ) ) ;
#10486=EDGE_CURVE ( 'NONE', #2677, #931, #9626, .T. ) ;
#10508=CARTESIAN_POINT ( 'NONE',  ( 0.000000000000000000, 0.000000000000000000, 0.000000000000000000 ) ) ;
#10510=CARTESIAN_POINT ( 'NONE',  ( -2.449848172108560540, -3.432307619358754724, -3.503702292528910078 ) ) ;
#10514=CARTESIAN_POINT ( 'NONE',  ( -3.436319922987618902, 2.634841920961291439, -3.531542292955721862 ) ) ;
#10538=ORIENTED_EDGE ( 'NONE', *, *, #5187, .F. ) ;
#10571=ORIENTED_EDGE ( 'NONE', *, *, #8685, .F. ) ;
#10573=CARTESIAN_POINT ( 'NONE',  ( -2.688821387764050996E-14, -4.618802153517012954, -0.4999999999999995559 ) ) ;
#10582=CARTESIAN_POINT ( 'NONE',  ( -0.6920835326022555245, -4.454600218803899558, -3.597382984111586079 ) ) ;
#10583=LINE ( 'NONE', #1494, #9322 ) ;
#10588=CARTESIAN_POINT ( 'NONE',  ( 0.1404048886732821022, 4.699864953788070565, -3.686887068327037387 ) ) ;
#10617=CARTESIAN_POINT ( 'NONE',  ( 5.384454397937118664, 0.000000000000000000, -5.000000000000000000 ) ) ;
#10647=CARTESIAN_POINT ( 'NONE',  ( -4.000000000000000000, -2.309401076758515803, -0.4999999999999995559 ) ) ;
#10661=CARTESIAN_POINT ( 'NONE',  ( -4.000000000000000000, 0.000000000000000000, 0.000000000000000000 ) ) ;
#10669=LINE ( 'NONE', #9582, #12574 ) ;
#10692=ORIENTED_EDGE ( 'NONE', *, *, #10486, .T. ) ;
#10704=ORIENTED_EDGE ( 'NONE', *, *, #5765, .T. ) ;
#10707=CIRCLE ( 'NONE', #2363, 2.500000000000000888 ) ;
#10715=B_SPLINE_CURVE_WITH_KNOTS ( 'NONE', 3,
 ( #13103, #14051, #3045, #14261, #975 ),
 .UNSPECIFIED., .F., .F.,
 ( 4, 1, 4 ),
 ( 5.640274452250024914E-20, 0.002309401076758505356, 0.004618802153517010713 ),
 .UNSPECIFIED. ) ;
#10734=CARTESIAN_POINT ( 'NONE',  ( 2.059999999999998721, 0.000000000000000000, -0.3080913168122742518 ) ) ;
#10735=( NAMED_UNIT ( * ) SI_UNIT ( $, .STERADIAN. ) SOLID_ANGLE_UNIT ( ) );
#10746=CARTESIAN_POINT ( 'NONE',  ( -3.511755186886750479, 2.826662030176366081, -3.597382984111578086 ) ) ;
#10774=CARTESIAN_POINT ( 'NONE',  ( 4.000000000000000000, -2.309401076758514915, -3.433295621305383349 ) ) ;
#10803=CARTESIAN_POINT ( 'NONE',  ( 4.211405965630455661, 2.460463115436283932, -3.751298928144577882 ) ) ;
#10814=CARTESIAN_POINT ( 'NONE',  ( -2.805705207896067144, 3.226868319750155312, -3.503898532754364581 ) ) ;
#10817=CARTESIAN_POINT ( 'NONE',  ( -4.000000000000000000, 1.941961291383472732, -0.3515519931180205448 ) ) ;
#10820=CARTESIAN_POINT ( 'NONE',  ( 0.000000000000000000, 0.000000000000000000, -4.484454397937119197 ) ) ;
#10828=ORIENTED_EDGE ( 'NONE', *, *, #10049, .T. ) ;
#10877=VECTOR ( 'NONE', #12660, 1000.000000000000114 ) ;
#10880=ORIENTED_EDGE ( 'NONE', *, *, #8818, .F. ) ;
#10897=FACE_OUTER_BOUND ( 'NONE', #8656, .T. ) ;
#10920=CIRCLE ( 'NONE', #13913, 5.560781378645573980 ) ;
#10925=PRODUCT_DEFINITION ( 'UNKNOWN', '', #7247, #6366 ) ;
#10928=AXIS2_PLACEMENT_3D ( 'NONE', #7561, #11859, #9611 ) ;
#10932=VECTOR ( 'NONE', #9551, 1000.000000000000000 ) ;
#10933=CARTESIAN_POINT ( 'NONE',  ( -4.211140560182196957, -2.431303136016552013, -3.745885042887436178 ) ) ;
#10938=EDGE_CURVE ( 'NONE', #5289, #8791, #6300, .T. ) ;
#10942=CONICAL_SURFACE ( 'NONE', #4686, 4.000000000000000000, 0.8911886515913786111 ) ;
#10945=CARTESIAN_POINT ( 'NONE',  ( 3.999999999999999112, -0.3979232138631231819, -5.929230630780099908E-17 ) ) ;
#10947=( LENGTH_UNIT ( ) NAMED_UNIT ( * ) SI_UNIT ( .MILLI., .METRE. ) );
#10959=B_SPLINE_CURVE_WITH_KNOTS ( 'NONE', 3,
 ( #11831, #11611, #1954, #11761 ),
 .UNSPECIFIED., .F., .F.,
 ( 4, 4 ),
 ( 0.000000000000000000, 0.002452478801916376308 ),
 .UNSPECIFIED. ) ;
#10960=EDGE_CURVE ( 'NONE', #924, #1149, #1985, .T. ) ;
#10965=FACE_OUTER_BOUND ( 'NONE', #7319, .T. ) ;
#10974=CARTESIAN_POINT ( 'NONE',  ( -4.000000000000000000, -2.512220745329312610, -3.469390707569719901 ) ) ;
#10983=ORIENTED_EDGE ( 'NONE', *, *, #11547, .T. ) ;
#10987=EDGE_CURVE ( 'NONE', #10282, #8744, #6095, .T. ) ;
#10991=VERTEX_POINT ( 'NONE', #12983 ) ;
#10997=FACE_OUTER_BOUND ( 'NONE', #12048, .T. ) ;
#11010=CARTESIAN_POINT ( 'NONE',  ( 4.000000000000000000, 0.000000000000000000, 0.000000000000000000 ) ) ;
#11022=DIRECTION ( 'NONE',  ( -0.000000000000000000, 0.000000000000000000, -1.000000000000000000 ) ) ;
#11033=EDGE_CURVE ( 'NONE', #3920, #8960, #8349, .T. ) ;
#11036=CARTESIAN_POINT ( 'NONE',  ( 5.560781378645573980, 6.809993116116507654E-16, -4.000000000000000000 ) ) ;
#11051=AXIS2_PLACEMENT_3D ( 'NONE', #8908, #27, #7869 ) ;
#11069=VERTEX_POINT ( 'NONE', #12039 ) ;
#11095=EDGE_LOOP ( 'NONE', ( #8692, #14227, #2451 ) ) ;
#11099=CARTESIAN_POINT ( 'NONE',  ( -4.000000000000000000, -0.7890432684750890990, -0.04868663549882315533 ) ) ;
#11110=CARTESIAN_POINT ( 'NONE',  ( -0.6666666666666666297, -4.233901974057276973, -3.300726591567087365 ) ) ;
#11115=ADVANCED_FACE ( 'NONE', ( #2094 ), #7174, .F. ) ;
#11126=CARTESIAN_POINT ( 'NONE',  ( 4.000000000000000000, 2.309401076758497151, -3.433295621305379353 ) ) ;
#11127=B_SPLINE_CURVE_WITH_KNOTS ( 'NONE', 3,
 ( #5938, #10290, #6011, #12472, #9063, #9132 ),
 .UNSPECIFIED., .F., .F.,
 ( 4, 2, 4 ),
 ( 0.002365888236227995517, 0.003551327329835084114, 0.004736766423442172712 ),
 .UNSPECIFIED. ) ;
#11153=DIRECTION ( 'NONE',  ( 0.8660254037844379305, 0.5000000000000013323, 0.000000000000000000 ) ) ;
#11156=EDGE_CURVE ( 'NONE', #2710, #4356, #946, .T. ) ;
#11181=CIRCLE ( 'NONE', #4691, 2.100000000000000089 ) ;
#11183=EDGE_CURVE ( 'NONE', #2006, #4356, #13558, .T. ) ;
#11192=DIRECTION ( 'NONE',  ( 1.000000000000000000, 0.000000000000000000, 0.000000000000000000 ) ) ;
#11197=CARTESIAN_POINT ( 'NONE',  ( 0.000000000000000000, 0.000000000000000000, 0.000000000000000000 ) ) ;
#11233=CARTESIAN_POINT ( 'NONE',  ( -4.000000000000000000, -0.3979232138631226823, -3.896351557369779711E-17 ) ) ;
#11240=CYLINDRICAL_SURFACE ( 'NONE', #7430, 2.100000000000000089 ) ;
#11284=ORIENTED_EDGE ( 'NONE', *, *, #3753, .F. ) ;
#11299=B_SPLINE_CURVE_WITH_KNOTS ( 'NONE', 3,
 ( #4514, #14295, #1969, #4231, #11989, #8652 ),
 .UNSPECIFIED., .F., .F.,
 ( 4, 2, 4 ),
 ( -3.640115492410698714E-06, 0.0002066546034003381217, 0.0004169493222930869755 ),
 .UNSPECIFIED. ) ;
#11308=CARTESIAN_POINT ( 'NONE',  ( 2.712762565639649015, -3.052587955997662306, -3.430618716626630871 ) ) ;
#11312=CARTESIAN_POINT ( 'NONE',  ( 3.540020015735602765, 2.810662092924382627, -3.602146406945867962 ) ) ;
#11316=CARTESIAN_POINT ( 'NONE',  ( -6.259644161404860030E-16, -4.618802153517027165, -3.433295621305388234 ) ) ;
#11323=VERTEX_POINT ( 'NONE', #11442 ) ;
#11336=CARTESIAN_POINT ( 'NONE',  ( -2.000000000000006661, 3.464101615137750834, 0.000000000000000000 ) ) ;
#11342=CARTESIAN_POINT ( 'NONE',  ( 0.000000000000000000, 0.000000000000000000, -0.3080913168122742518 ) ) ;
#11344=ORIENTED_EDGE ( 'NONE', *, *, #3325, .F. ) ;
#11346=VERTEX_POINT ( 'NONE', #10429 ) ;
#11348=FACE_OUTER_BOUND ( 'NONE', #6461, .T. ) ;
#11355=CARTESIAN_POINT ( 'NONE',  ( -2.500000000000000888, 0.000000000000000000, -4.974599999999998801 ) ) ;
#11369=AXIS2_PLACEMENT_3D ( 'NONE', #6595, #11022, #1052 ) ;
#11371=VERTEX_POINT ( 'NONE', #6513 ) ;
#11379=CARTESIAN_POINT ( 'NONE',  ( 0.6810597143197052450, 4.461075778259290914, -3.598441714920602053 ) ) ;
#11427=B_SPLINE_CURVE_WITH_KNOTS ( 'NONE', 3,
 ( #1883, #10746, #10814, #9365, #13776, #3843, #2760, #6930 ),
 .UNSPECIFIED., .F., .F.,
 ( 4, 2, 2, 4 ),
 ( 0.000000000000000000, 0.002450665683189820997, 0.003675998524784731495, 0.004901331366379641993 ),
 .UNSPECIFIED. ) ;
#11428=DIRECTION ( 'NONE',  ( 0.000000000000000000, -0.000000000000000000, 1.000000000000000000 ) ) ;
#11442=CARTESIAN_POINT ( 'NONE',  ( -4.000000000000000000, 2.309401076758498483, -0.4999999999999927280 ) ) ;
#11446=CARTESIAN_POINT ( 'NONE',  ( 3.453038570460273071, 2.625189405340834448, -3.535263753543585352 ) ) ;
#11449=DIRECTION ( 'NONE',  ( 0.000000000000000000, 0.000000000000000000, 1.000000000000000000 ) ) ;
#11468=ORIENTED_EDGE ( 'NONE', *, *, #13667, .T. ) ;
#11481=CARTESIAN_POINT ( 'NONE',  ( 1.567478505476134606E-15, 4.618802153517012066, -3.433295621305382905 ) ) ;
#11482=ORIENTED_EDGE ( 'NONE', *, *, #8607, .T. ) ;
#11488=CARTESIAN_POINT ( 'NONE',  ( 0.000000000000000000, 0.000000000000000000, -5.000000000000000888 ) ) ;
#11500=DIRECTION ( 'NONE',  ( -0.000000000000000000, -0.000000000000000000, 1.000000000000000000 ) ) ;
#11503=EDGE_LOOP ( 'NONE', ( #5542, #3218, #911, #7340 ) ) ;
#11508=FACE_OUTER_BOUND ( 'NONE', #11701, .T. ) ;
#11520=CARTESIAN_POINT ( 'NONE',  ( 0.02511973781850649831, -4.877415612947427981, -3.751298745799844792 ) ) ;
#11537=ORIENTED_EDGE ( 'NONE', *, *, #9775, .F. ) ;
#11540=DIRECTION ( 'NONE',  ( -1.000000000000000000, 0.000000000000000000, 0.000000000000000000 ) ) ;
#11547=EDGE_CURVE ( 'NONE', #8744, #10991, #10920, .T. ) ;
#11548=CARTESIAN_POINT ( 'NONE',  ( -4.000000000000000000, 2.309401076758498483, -3.433295621305379353 ) ) ;
#11553=CARTESIAN_POINT ( 'NONE',  ( 4.000000000000000000, -2.309401076758516691, -0.4999999999999995559 ) ) ;
#11564=AXIS2_PLACEMENT_3D ( 'NONE', #13541, #2395, #1570 ) ;
#11588=EDGE_CURVE ( 'NONE', #1964, #4974, #13679, .T. ) ;
#11602=AXIS2_PLACEMENT_3D ( 'NONE', #7660, #7795, #12231 ) ;
#11611=CARTESIAN_POINT ( 'NONE',  ( -4.203833317240879275, -1.627343821129593859, -3.597273115243890818 ) ) ;
#11622=ORIENTED_EDGE ( 'NONE', *, *, #6581, .T. ) ;
#11636=DIRECTION ( 'NONE',  ( 0.000000000000000000, -0.000000000000000000, 1.000000000000000000 ) ) ;
#11672=CARTESIAN_POINT ( 'NONE',  ( -2.712762565639006418, 3.052587955997511759, -3.430618716626627318 ) ) ;
#11689=SHAPE_DEFINITION_REPRESENTATION ( #3685, #9307 ) ;
#11698=CARTESIAN_POINT ( 'NONE',  ( 2.345747346278113987, -3.264484291692503870, -0.01223254789874484924 ) ) ;
#11701=EDGE_LOOP ( 'NONE', ( #8295, #3005, #3944, #4661, #7488 ) ) ;
#11714=AXIS2_PLACEMENT_3D ( 'NONE', #6826, #5535, #5738 ) ;
#11733=CARTESIAN_POINT ( 'NONE',  ( -0.3198814748697807464, -4.434118497892185040, -0.3507732604232532969 ) ) ;
#11745=CARTESIAN_POINT ( 'NONE',  ( -1.257172072275743346, 3.892973519171203378, -3.433252694550776862 ) ) ;
#11747=EDGE_LOOP ( 'NONE', ( #12871, #2761, #12112, #1439 ) ) ;
#11749=CARTESIAN_POINT ( 'NONE',  ( 8.673617379884035472E-16, 4.618802153517012954, -5.000000000000000000 ) ) ;
#11756=ORIENTED_EDGE ( 'NONE', *, *, #4171, .F. ) ;
#11761=CARTESIAN_POINT ( 'NONE',  ( -4.197393957002303999, -7.773935952363655451E-14, -3.503767560748929810 ) ) ;
#11764=EDGE_CURVE ( 'NONE', #2488, #12837, #139, .T. ) ;
#11795=ORIENTED_EDGE ( 'NONE', *, *, #2300, .T. ) ;
#11814=FACE_OUTER_BOUND ( 'NONE', #7449, .T. ) ;
#11831=CARTESIAN_POINT ( 'NONE',  ( -4.211140560182196957, -2.431303136016552013, -3.745885042887436178 ) ) ;
#11847=ORIENTED_EDGE ( 'NONE', *, *, #12224, .F. ) ;
#11849=CARTESIAN_POINT ( 'NONE',  ( 2.000000000000005329, -3.464101615137751722, 0.000000000000000000 ) ) ;
#11850=ORIENTED_EDGE ( 'NONE', *, *, #9850, .T. ) ;
#11859=DIRECTION ( 'NONE',  ( -0.000000000000000000, 0.000000000000000000, -1.000000000000000000 ) ) ;
#11876=DIRECTION ( 'NONE',  ( -0.000000000000000000, -0.000000000000000000, 1.000000000000000000 ) ) ;
#11884=CARTESIAN_POINT ( 'NONE',  ( 0.3461262719736147297, -4.658553426539303821, -3.671615880910379381 ) ) ;
#11894=AXIS2_PLACEMENT_3D ( 'NONE', #5304, #697, #8475 ) ;
#11896=EDGE_LOOP ( 'NONE', ( #9432, #10704, #11468, #10828, #9932 ) ) ;
#11914=CARTESIAN_POINT ( 'NONE',  ( -3.999999999998910649, -1.658469974638591804, -3.531532913075256186 ) ) ;
#11921=ADVANCED_FACE ( 'NONE', ( #14101 ), #12649, .T. ) ;
#11953=CARTESIAN_POINT ( 'NONE',  ( 0.000000000000000000, 0.000000000000000000, -5.000000000000000000 ) ) ;
#11961=EDGE_LOOP ( 'NONE', ( #11284, #10538, #13777, #11482 ) ) ;
#11966=CARTESIAN_POINT ( 'NONE',  ( 0.000000000000000000, 0.000000000000000000, 3.469446951953614189E-15 ) ) ;
#11970=ORIENTED_EDGE ( 'NONE', *, *, #5693, .F. ) ;
#11989=CARTESIAN_POINT ( 'NONE',  ( -4.000000000000003553, 2.309401076758496263, -3.504269196027868905 ) ) ;
#12027=CONICAL_SURFACE ( 'NONE', #4608, 2.500000000000000888, 0.9599310885968785900 ) ;
#12028=ORIENTED_EDGE ( 'NONE', *, *, #894, .T. ) ;
#12039=CARTESIAN_POINT ( 'NONE',  ( 2.500000000000000888, 3.061616997868384127E-16, -4.974599999999998801 ) ) ;
#12048=EDGE_LOOP ( 'NONE', ( #3035, #5806, #5500 ) ) ;
#12073=EDGE_CURVE ( 'NONE', #2710, #2006, #2923, .T. ) ;
#12075=ORIENTED_EDGE ( 'NONE', *, *, #11764, .T. ) ;
#12081=CARTESIAN_POINT ( 'NONE',  ( -3.679171394226034675, -2.494631558665844739, -0.3503314178412558211 ) ) ;
#12092=EDGE_CURVE ( 'NONE', #11346, #1964, #2138, .T. ) ;
#12112=ORIENTED_EDGE ( 'NONE', *, *, #14237, .T. ) ;
#12118=CARTESIAN_POINT ( 'NONE',  ( -2.000000000000007550, -3.464101615137749945, 0.000000000000000000 ) ) ;
#12122=DIRECTION ( 'NONE',  ( -1.000000000000000000, 0.000000000000000000, 0.000000000000000000 ) ) ;
#12145=CARTESIAN_POINT ( 'NONE',  ( -6.473970235329672780E-16, -4.862606272033106691, -3.745885042887442395 ) ) ;
#12151=ADVANCED_BREP_SHAPE_REPRESENTATION ( '', ( #8769, #14039 ), #1206 ) ;
#12152=ORIENTED_EDGE ( 'NONE', *, *, #4639, .T. ) ;
#12171=CARTESIAN_POINT ( 'NONE',  ( 3.333333333333332593, 2.694301256218250007, -3.300726591567078483 ) ) ;
#12202=CARTESIAN_POINT ( 'NONE',  ( 4.000000000000000000, -2.309401076758514915, -3.433295621305383349 ) ) ;
#12224=EDGE_CURVE ( 'NONE', #11346, #2397, #4328, .T. ) ;
#12231=DIRECTION ( 'NONE',  ( 1.000000000000000000, 0.000000000000000000, 0.000000000000000000 ) ) ;
#12235=CARTESIAN_POINT ( 'NONE',  ( 1.312671235360372224, 3.860931062424219462, -0.05923475698270440348 ) ) ;
#12249=CARTESIAN_POINT ( 'NONE',  ( -4.000000000000000000, -2.309401076758515803, -0.4999999999999995559 ) ) ;
#12254=LINE ( 'NONE', #7535, #6634 ) ;
#12262=DIRECTION ( 'NONE',  ( 0.000000000000000000, 0.000000000000000000, -1.000000000000000000 ) ) ;
#12268=ORIENTED_EDGE ( 'NONE', *, *, #12980, .T. ) ;
#12271=EDGE_CURVE ( 'NONE', #3312, #11069, #12573, .T. ) ;
#12290=ORIENTED_EDGE ( 'NONE', *, *, #1798, .T. ) ;
#12293=CARTESIAN_POINT ( 'NONE',  ( 0.000000000000000000, 0.000000000000000000, 0.000000000000000000 ) ) ;
#12306=CARTESIAN_POINT ( 'NONE',  ( 0.000000000000000000, 0.000000000000000000, -4.000000000000000000 ) ) ;
#12309=EDGE_LOOP ( 'NONE', ( #12756, #10692, #4030, #4378, #102 ) ) ;
#12319=CARTESIAN_POINT ( 'NONE',  ( 0.5276280594147412240, -4.314175951381924889, -3.320322319201654881 ) ) ;
#12343=VERTEX_POINT ( 'NONE', #4082 ) ;
#12344=CARTESIAN_POINT ( 'NONE',  ( 0.000000000000000000, 0.000000000000000000, -5.000000000000000000 ) ) ;
#12402=ORIENTED_EDGE ( 'NONE', *, *, #9850, .F. ) ;
#12412=CARTESIAN_POINT ( 'NONE',  ( -4.000000000000000000, 2.309401076758498483, -3.433295621305379353 ) ) ;
#12422=FACE_OUTER_BOUND ( 'NONE', #9213, .T. ) ;
#12466=CARTESIAN_POINT ( 'NONE',  ( -2.742827927723112236, -3.035229711105190464, -3.433252694550595230 ) ) ;
#12472=CARTESIAN_POINT ( 'NONE',  ( 3.349226789952652439, 2.685125164760731487, -0.2236248678334773199 ) ) ;
#12488=SURFACE_STYLE_FILL_AREA ( #5023 ) ;
#12532=CARTESIAN_POINT ( 'NONE',  ( -1.312671235360383548, -3.860931062424228788, -0.05923475698271369466 ) ) ;
#12539=CARTESIAN_POINT ( 'NONE',  ( -1.274258131565027874, -3.883108878240886241, -3.220599429844051009 ) ) ;
#12553=ORIENTED_EDGE ( 'NONE', *, *, #2670, .F. ) ;
#12562=DIRECTION ( 'NONE',  ( -0.000000000000000000, -0.000000000000000000, 1.000000000000000000 ) ) ;
#12564=( LENGTH_UNIT ( ) NAMED_UNIT ( * ) SI_UNIT ( .MILLI., .METRE. ) );
#12573=LINE ( 'NONE', #9237, #1536 ) ;
#12574=VECTOR ( 'NONE', #6163, 1000.000000000000227 ) ;
#12575=ORIENTED_EDGE ( 'NONE', *, *, #10049, .F. ) ;
#12587=CARTESIAN_POINT ( 'NONE',  ( 0.3208286057739604957, -4.433571671609698228, -0.3503314178412692548 ) ) ;
#12589=FACE_OUTER_BOUND ( 'NONE', #7264, .T. ) ;
#12615=CARTESIAN_POINT ( 'NONE',  ( 4.101954839143203912, -2.368264730583031330, -3.681130640444377988 ) ) ;
#12623=DIRECTION ( 'NONE',  ( -1.000000000000000000, 0.000000000000000000, 0.000000000000000000 ) ) ;
#12637=EDGE_LOOP ( 'NONE', ( #8739, #13033, #10154, #6134, #9231, #12290, #10983 ) ) ;
#12649=CONICAL_SURFACE ( 'NONE', #1290, 5.560781378645573980, 1.221730476396046816 ) ;
#12652=CARTESIAN_POINT ( 'NONE',  ( -2.500000000000000888, 0.000000000000000000, -4.974599999999998801 ) ) ;
#12660=DIRECTION ( 'NONE',  ( 0.8191520442889902442, 1.003171929053522651E-16, -0.5735764363510482688 ) ) ;
#12702=DIRECTION ( 'NONE',  ( 1.000000000000000000, 0.000000000000000000, 0.000000000000000000 ) ) ;
#12728=CARTESIAN_POINT ( 'NONE',  ( 2.000000000000005329, -3.464101615137751722, 0.000000000000000000 ) ) ;
#12729=CIRCLE ( 'NONE', #10184, 2.500000000000000444 ) ;
#12731=( BOUNDED_SURFACE ( )  B_SPLINE_SURFACE ( 3, 2, ( 
 ( #1869, #760, #5220 ),
 ( #9639, #4129, #8545 ),
 ( #12973, #3046, #6371 ),
 ( #834, #4607, #13245 ),
 ( #1254, #7994, #6787 ),
 ( #3455, #6850, #10803 ) ),
 .UNSPECIFIED., .F., .F., .F. ) 
 B_SPLINE_SURFACE_WITH_KNOTS ( ( 4, 2, 4 ),
 ( 3, 3 ),
 ( 0.02027065861071770947, 0.02273072267836921331, 0.02519078674602071716 ),
 ( 0.000000000000000000, 1.000000000000000000 ),
 .UNSPECIFIED. ) 
 GEOMETRIC_REPRESENTATION_ITEM ( )  RATIONAL_B_SPLINE_SURFACE ( (
 ( 1.000000000000000000, 0.8047781708337304885, 1.000000000000000000),
 ( 1.000000000000000000, 0.8123765190705307671, 1.000000000000000000),
 ( 1.000000000000000000, 0.8190656277163975707, 1.000000000000000000),
 ( 1.000000000000000000, 0.8192366903512159348, 1.000000000000000000),
 ( 1.000000000000000000, 0.8126138454302893610, 1.000000000000000000),
 ( 1.000000000000000000, 0.8047712246031417660, 1.000000000000000000) ) ) 
 REPRESENTATION_ITEM ( '' )  SURFACE ( )  );
#12743=CARTESIAN_POINT ( 'NONE',  ( 1.411581201560190495E-15, 4.862606272033091592, -3.745885042887436622 ) ) ;
#12754=CARTESIAN_POINT ( 'NONE',  ( -3.522875095019672109, 2.820352903225427532, -3.598441714920591394 ) ) ;
#12756=ORIENTED_EDGE ( 'NONE', *, *, #13667, .F. ) ;
#12772=UNCERTAINTY_MEASURE_WITH_UNIT (LENGTH_MEASURE( 1.000000000000000082E-05 ), #9225, 'distance_accuracy_value', 'NONE');
#12779=CARTESIAN_POINT ( 'NONE',  ( -3.333333333333335258, 2.694301256218251783, -3.300726591567079815 ) ) ;
#12787=CARTESIAN_POINT ( 'NONE',  ( 3.355112389629172576, -2.681727112203168950, -0.2256878752776777242 ) ) ;
#12798=EDGE_CURVE ( 'NONE', #931, #2006, #13850, .T. ) ;
#12812=DIRECTION ( 'NONE',  ( 0.000000000000000000, 0.000000000000000000, -1.000000000000000000 ) ) ;
#12820=CARTESIAN_POINT ( 'NONE',  ( -2.000000000000007550, -3.464101615137749945, 0.000000000000000000 ) ) ;
#12821=EDGE_CURVE ( 'NONE', #6723, #11371, #9835, .T. ) ;
#12826=CARTESIAN_POINT ( 'NONE',  ( -1.391697335622809950, -4.043246145443391448, -3.503898532754372575 ) ) ;
#12828=CARTESIAN_POINT ( 'NONE',  ( -4.141042297810615835, 2.227970268150415656, -3.687027686973619822 ) ) ;
#12837=VERTEX_POINT ( 'NONE', #9651 ) ;
#12843=CARTESIAN_POINT ( 'NONE',  ( 4.197393957002303999, 7.772902908466098641E-14, -3.503767560748929810 ) ) ;
#12868=CARTESIAN_POINT ( 'NONE',  ( -4.000000000000000888, -1.539600717839011201, -3.300726591567081591 ) ) ;
#12871=ORIENTED_EDGE ( 'NONE', *, *, #12092, .F. ) ;
#12873=DIRECTION ( 'NONE',  ( -1.000000000000000000, 0.000000000000000000, 0.000000000000000000 ) ) ;
#12883=ORIENTED_EDGE ( 'NONE', *, *, #2723, .T. ) ;
#12886=DIRECTION ( 'NONE',  ( 0.000000000000000000, 0.000000000000000000, 1.000000000000000000 ) ) ;
#12910=ORIENTED_EDGE ( 'NONE', *, *, #12271, .F. ) ;
#12916=ORIENTED_EDGE ( 'NONE', *, *, #9139, .T. ) ;
#12952=AXIS2_PLACEMENT_3D ( 'NONE', #13783, #12562, #8195 ) ;
#12953=EDGE_CURVE ( 'NONE', #11371, #924, #11427, .T. ) ;
#12973=CARTESIAN_POINT ( 'NONE',  ( 4.000000000000000000, -0.8732470631449981147, -3.223155494240760088 ) ) ;
#12980=EDGE_CURVE ( 'NONE', #6984, #10102, #7937, .T. ) ;
#12983=CARTESIAN_POINT ( 'NONE',  ( 5.560781378645575757, 0.000000000000000000, -4.000000000000000000 ) ) ;
#12988=CARTESIAN_POINT ( 'NONE',  ( -4.197393957002303999, -7.773935952363655451E-14, -3.503767560748929810 ) ) ;
#12997=CARTESIAN_POINT ( 'NONE',  ( 1.734723475976807094E-15, 4.618802153517012954, -0.4999999999999995559 ) ) ;
#13033=ORIENTED_EDGE ( 'NONE', *, *, #4126, .T. ) ;
#13093=ADVANCED_FACE ( 'NONE', ( #12589 ), #1085, .T. ) ;
#13103=CARTESIAN_POINT ( 'NONE',  ( -6.259644161404860030E-16, -4.618802153517027165, -3.433295621305388234 ) ) ;
#13115=EDGE_CURVE ( 'NONE', #11346, #2351, #5914, .T. ) ;
#13121=CARTESIAN_POINT ( 'NONE',  ( -3.540020015735593439, -2.810662092924100630, -3.602146406945814672 ) ) ;
#13131=CARTESIAN_POINT ( 'NONE',  ( -0.3208286057739654917, 4.433571671609680465, -0.3503314178412548774 ) ) ;
#13204=DIRECTION ( 'NONE',  ( 0.000000000000000000, 0.000000000000000000, -1.000000000000000000 ) ) ;
#13207=CARTESIAN_POINT ( 'NONE',  ( -4.203934362469166963, -1.640673743454851286, -3.598432614606932756 ) ) ;
#13213=ORIENTED_EDGE ( 'NONE', *, *, #9139, .F. ) ;
#13238=CARTESIAN_POINT ( 'NONE',  ( 3.511755186886750923, -2.826662030176382956, -3.597382984111582083 ) ) ;
#13245=CARTESIAN_POINT ( 'NONE',  ( 4.197310751797292738, 0.8178363989516252985, -3.502498386812444409 ) ) ;
#13290=CARTESIAN_POINT ( 'NONE',  ( 4.000000000000000000, -1.084202172485504434E-14, -3.142992957459231906 ) ) ;
#13295=ORIENTED_EDGE ( 'NONE', *, *, #12953, .T. ) ;
#13315=ADVANCED_FACE ( 'NONE', ( #10997 ), #864, .T. ) ;
#13351=AXIS2_PLACEMENT_3D ( 'NONE', #11488, #11636, #8363 ) ;
#13376=CARTESIAN_POINT ( 'NONE',  ( 2.100000000000000089, 0.000000000000000000, -4.694516984716113228 ) ) ;
#13383=CARTESIAN_POINT ( 'NONE',  ( 4.000000000000000000, 2.309401076758497151, -5.000000000000000000 ) ) ;
#13395=VERTEX_POINT ( 'NONE', #2788 ) ;
#13429=EDGE_LOOP ( 'NONE', ( #2640, #2567, #2133, #3859 ) ) ;
#13451=DIRECTION ( 'NONE',  ( -0.000000000000000000, -0.000000000000000000, 1.000000000000000000 ) ) ;
#13452=CARTESIAN_POINT ( 'NONE',  ( 4.000000000000000000, 2.309401076758515803, -0.4999999999999995559 ) ) ;
#13455=ADVANCED_FACE ( 'NONE', ( #11348 ), #9465, .T. ) ;
#13463=AXIS2_PLACEMENT_3D ( 'NONE', #11966, #4059, #13986 ) ;
#13464=CARTESIAN_POINT ( 'NONE',  ( 3.436319922986518449, -2.634841920959471562, -3.531542292954761741 ) ) ;
#13516=DIRECTION ( 'NONE',  ( -1.000000000000000000, 0.000000000000000000, 0.000000000000000000 ) ) ;
#13527=CARTESIAN_POINT ( 'NONE',  ( 0.6666666666666689611, 4.233901974057261874, -3.300726591567082480 ) ) ;
#13529=CARTESIAN_POINT ( 'NONE',  ( 0.5469614295415388128, -4.303013824935362663, -3.535263753543555598 ) ) ;
#13541=CARTESIAN_POINT ( 'NONE',  ( 5.384454397937118664, 0.000000000000000000, -4.484454397937119197 ) ) ;
#13558=B_SPLINE_CURVE_WITH_KNOTS ( 'NONE', 3,
 ( #12249, #4425, #6806, #11099, #11233, #3348 ),
 .UNSPECIFIED., .F., .F.,
 ( 4, 2, 4 ),
 ( 0.003358874760055550156, 0.004541967308452096383, 0.005725059856848641743 ),
 .UNSPECIFIED. ) ;
#13563=( NAMED_UNIT ( * ) PLANE_ANGLE_UNIT ( ) SI_UNIT ( $, .RADIAN. ) );
#13579=CARTESIAN_POINT ( 'NONE',  ( 3.999999999999999112, -0.7890432684750902093, -0.04868663549882291247 ) ) ;
#13617=CARTESIAN_POINT ( 'NONE',  ( -4.000000000000000000, -2.309401076758512694, -3.433295621305382461 ) ) ;
#13632=DIRECTION ( 'NONE',  ( 0.000000000000000000, 0.000000000000000000, -1.000000000000000000 ) ) ;
#13653=DIRECTION ( 'NONE',  ( -0.000000000000000000, -0.000000000000000000, 1.000000000000000000 ) ) ;
#13664=PLANE ( 'NONE',  #5677 ) ;
#13667=EDGE_CURVE ( 'NONE', #2677, #11323, #9535, .T. ) ;
#13679=CIRCLE ( 'NONE', #11602, 2.100000000000000089 ) ;
#13691=CARTESIAN_POINT ( 'NONE',  ( -2.855764796983342624, 2.970025579236414082, -0.09382832055445475272 ) ) ;
#13708=CONICAL_SURFACE ( 'NONE', #2145, 4.000000000000000000, 0.8911886515913786111 ) ;
#13711=CARTESIAN_POINT ( 'NONE',  ( -3.264624719419710521E-13, -4.796980096169328966, -3.721999068284310486 ) ) ;
#13724=EDGE_CURVE ( 'NONE', #5289, #6984, #6295, .T. ) ;
#13725=DIRECTION ( 'NONE',  ( -1.000000000000000000, 0.000000000000000000, 0.000000000000000000 ) ) ;
#13726=COLOUR_RGB ( '',1.000000000000000000, 0.9490196078431372140, 0.9098039215686274384 ) ;
#13737=VERTEX_POINT ( 'NONE', #9964 ) ;
#13738=ORIENTED_EDGE ( 'NONE', *, *, #3116, .F. ) ;
#13747=CARTESIAN_POINT ( 'NONE',  ( -6.259644161404860030E-16, -4.618802153517027165, -5.000000000000000000 ) ) ;
#13762=CARTESIAN_POINT ( 'NONE',  ( -3.355112389629170799, 2.681727112203152963, -0.2256878752776689534 ) ) ;
#13764=CLOSED_SHELL ( 'NONE', ( #2685, #4027, #2033, #5439, #13455, #3145, #1042, #5216, #4674, #5690, #7849, #9976, #2416, #4106, #416, #8469, #11921, #7053, #13315, #10205, #9598, #2483, #13093, #14275, #11115, #5879, #3328, #4258, #7712, #1237, #13847, #2066 ) ) ;
#13776=CARTESIAN_POINT ( 'NONE',  ( -1.393927851585477606, 4.043713361053528743, -3.526374918436835149 ) ) ;
#13777=ORIENTED_EDGE ( 'NONE', *, *, #12271, .T. ) ;
#13783=CARTESIAN_POINT ( 'NONE',  ( 0.000000000000000000, 0.000000000000000000, -25.03750572909317285 ) ) ;
#13797=CONICAL_SURFACE ( 'NONE', #1504, 4.000000000000000000, 0.8911886515913786111 ) ;
#13799=CARTESIAN_POINT ( 'NONE',  ( 1.411581201560190495E-15, 4.862606272033091592, -3.745885042887436622 ) ) ;
#13809=CARTESIAN_POINT ( 'NONE',  ( 0.000000000000000000, 0.000000000000000000, -4.000000000000000000 ) ) ;
#13817=EDGE_CURVE ( 'NONE', #6984, #2940, #2501, .T. ) ;
#13838=CARTESIAN_POINT ( 'NONE',  ( 4.000000000000000000, 0.9868501483902631932, -0.09357334158579604100 ) ) ;
#13847=ADVANCED_FACE ( 'NONE', ( #271 ), #9447, .F. ) ;
#13850=LINE ( 'NONE', #6310, #5972 ) ;
#13854=CARTESIAN_POINT ( 'NONE',  ( -4.000000000000000000, 2.309401076758498483, -0.4999999999999927280 ) ) ;
#13860=CARTESIAN_POINT ( 'NONE',  ( 1.567478505476134606E-15, 4.618802153517012066, -3.433295621305382905 ) ) ;
#13871=DIRECTION ( 'NONE',  ( -1.000000000000000000, 0.000000000000000000, 0.000000000000000000 ) ) ;
#13874=LINE ( 'NONE', #3950, #1648 ) ;
#13907=DIRECTION ( 'NONE',  ( -0.8191520442889875797, 1.003171929053519570E-16, 0.5735764363510522656 ) ) ;
#13913=AXIS2_PLACEMENT_3D ( 'NONE', #12306, #13451, #4543 ) ;
#13919=DIRECTION ( 'NONE',  ( 0.000000000000000000, 0.000000000000000000, 1.000000000000000000 ) ) ;
#13946=CARTESIAN_POINT ( 'NONE',  ( -4.000000000000000000, 2.309401076758498483, -5.000000000000000000 ) ) ;
#13947=CARTESIAN_POINT ( 'NONE',  ( 3.510273485745307731, 2.827716139362654424, -3.610536846335885564 ) ) ;
#13955=ORIENTED_EDGE ( 'NONE', *, *, #3623, .F. ) ;
#13976=ORIENTED_EDGE ( 'NONE', *, *, #9965, .T. ) ;
#13979=CARTESIAN_POINT ( 'NONE',  ( -3.861362476283256129, -2.629030857716004199, -3.671615880910374941 ) ) ;
#13981=CARTESIAN_POINT ( 'NONE',  ( -2.725741868435985094, 3.045094352034055429, -3.220599429844047012 ) ) ;
#13986=DIRECTION ( 'NONE',  ( 1.000000000000000000, 0.000000000000000000, 0.000000000000000000 ) ) ;
#13999=EDGE_CURVE ( 'NONE', #4356, #11323, #1268, .T. ) ;
#14027=EDGE_CURVE ( 'NONE', #14086, #6723, #10959, .T. ) ;
#14039=AXIS2_PLACEMENT_3D ( 'NONE', #10508, #9418, #5077 ) ;
#14051=CARTESIAN_POINT ( 'NONE',  ( 0.6666666666666658525, -4.233901974057276085, -3.300726591567086476 ) ) ;
#14073=VECTOR ( 'NONE', #7865, 1000.000000000000000 ) ;
#14074=CARTESIAN_POINT ( 'NONE',  ( 4.197393957002303999, 0.8151795401431359833, -3.503767560748935139 ) ) ;
#14080=EDGE_LOOP ( 'NONE', ( #10141, #8232 ) ) ;
#14086=VERTEX_POINT ( 'NONE', #706 ) ;
#14101=FACE_OUTER_BOUND ( 'NONE', #12637, .T. ) ;
#14135=CARTESIAN_POINT ( 'NONE',  ( -4.000000000000000000, 0.9868501483902560878, -0.09357334158579519445 ) ) ;
#14144=CARTESIAN_POINT ( 'NONE',  ( -4.211405944401398038, -2.460460786169389902, -3.751298493805494072 ) ) ;
#14169=DIRECTION ( 'NONE',  ( -1.000000000000000000, 0.000000000000000000, 0.000000000000000000 ) ) ;
#14184=ORIENTED_EDGE ( 'NONE', *, *, #8818, .T. ) ;
#14189=DIRECTION ( 'NONE',  ( -1.000000000000000000, 0.000000000000000000, 0.000000000000000000 ) ) ;
#14191=ORIENTED_EDGE ( 'NONE', *, *, #5693, .T. ) ;
#14204=ORIENTED_EDGE ( 'NONE', *, *, #10960, .T. ) ;
#14208=( BOUNDED_SURFACE ( )  B_SPLINE_SURFACE ( 3, 2, ( 
 ( #3552, #2453, #6876 ),
 ( #4928, #11446, #11312 ),
 ( #249, #5863, #10355 ),
 ( #10432, #3615, #3481 ),
 ( #8025, #6948, #11379 ),
 ( #1429, #10285, #9198 ) ),
 .UNSPECIFIED., .F., .F., .F. ) 
 B_SPLINE_SURFACE_WITH_KNOTS ( ( 4, 2, 4 ),
 ( 3, 3 ),
 ( 0.02032853247518126225, 0.02278863295364821212, 0.02524873343211516200 ),
 ( 0.000000000000000000, 1.000000000000000000 ),
 .UNSPECIFIED. ) 
 GEOMETRIC_REPRESENTATION_ITEM ( )  RATIONAL_B_SPLINE_SURFACE ( (
 ( 1.000000000000000000, 0.8047781615896835161, 1.000000000000000000),
 ( 1.000000000000000000, 0.8123767586291043008, 1.000000000000000000),
 ( 1.000000000000000000, 0.8190662415562011134, 1.000000000000000000),
 ( 1.000000000000000000, 0.8192361015671398849, 1.000000000000000000),
 ( 1.000000000000000000, 0.8126135807102121689, 1.000000000000000000),
 ( 1.000000000000000000, 0.8047712338318585568, 1.000000000000000000) ) ) 
 REPRESENTATION_ITEM ( '' )  SURFACE ( )  );
#14227=ORIENTED_EDGE ( 'NONE', *, *, #8942, .T. ) ;
#14229=CARTESIAN_POINT ( 'NONE',  ( 4.101954839143203912, 2.368264730583012234, -3.681130640444374436 ) ) ;
#14231=DIRECTION ( 'NONE',  ( 0.000000000000000000, 0.000000000000000000, -1.000000000000000000 ) ) ;
#14237=EDGE_CURVE ( 'NONE', #2397, #4974, #12254, .T. ) ;
#14241=CARTESIAN_POINT ( 'NONE',  ( 4.211140560182196957, -2.431303136016555122, -3.745885042887436622 ) ) ;
#14257=CARTESIAN_POINT ( 'NONE',  ( 1.654252653721905331, 3.663718938583014229, -0.01223254789873410957 ) ) ;
#14261=CARTESIAN_POINT ( 'NONE',  ( 3.333333333333335702, -2.694301256218268215, -3.300726591567084256 ) ) ;
#14275=ADVANCED_FACE ( 'NONE', ( #10965 ), #2358, .F. ) ;
#14277=CARTESIAN_POINT ( 'NONE',  ( -3.472371940586054251, -2.614027278893156669, -3.320322319202162031 ) ) ;
#14280=CARTESIAN_POINT ( 'NONE',  ( 4.211140560182196957, 2.431303136016536470, -3.745885042887433514 ) ) ;
#14284=PLANE ( 'NONE',  #1115 ) ;
#14295=CARTESIAN_POINT ( 'NONE',  ( -4.154094228333542915, 2.398367420968061658, -3.721909803043254694 ) ) ;
#14411=COLOUR_RGB('Black',0.12,0.14,0.17);
#14412=FILL_AREA_STYLE_COLOUR('',#14411);
#14413=FILL_AREA_STYLE('',(#14412));
#14414=SURFACE_STYLE_FILL_AREA(#14413);
#14415=SURFACE_SIDE_STYLE('',(#14414));
#14416=SURFACE_STYLE_USAGE(.BOTH.,#14415);
#14417=PRESENTATION_STYLE_ASSIGNMENT((#14416));
ENDSEC;
END-ISO-10303-21;
